ISO-10303-21;
HEADER;
/* Generated by software containing ST-Developer
 * from STEP Tools, Inc. (www.steptools.com) 
 */

FILE_DESCRIPTION(
/* description */ ('Independent maintained push-to-latch/pull-to-reset mushroom-operator 
CAD. Two opposed spring-loaded ball detents in turned circular seats b
ias both travel stops; direct normally-closed bridge opens6mm when pre
ssed. Rounded palm/pull rim, captured head screw, removable detent clo
sures, native Coil spring families, insulated shared terminals and ord
inary machining features. Manual geometric states and ideal same-mater
ial spring-energy direction only; no electrical/safety certification, 
force/contact dynamics, wear, load or life rating. Requested blue/gray
 visual palette, not safety identification. External wiring/anchors an
d application engineering omitted.'),
/* implementation_level */ '2;1');

FILE_NAME(
/* name */ 'Socket head cap screw M4x12.step',
/* time_stamp */ '2026-11-08T17:54:26-08:00',
/* author */ (''),
/* organization */ (''),
/* preprocessor_version */ 'ST-DEVELOPER v20.2',
/* originating_system */ 'Autodesk Translation Framework v15.17.0.0',
/* authorisation */ '');

FILE_SCHEMA (('AUTOMOTIVE_DESIGN { 1 0 10303 214 3 1 1 }'));
ENDSEC;

DATA;
#10=MECHANICAL_DESIGN_GEOMETRIC_PRESENTATION_REPRESENTATION('',(#203),#43980);
#147=CONICAL_SURFACE('',#12088,0.15,0.785398163397449);
#169=SHAPE_REPRESENTATION_RELATIONSHIP('SRR','None',#44069,#186);
#186=ADVANCED_BREP_SHAPE_REPRESENTATION('',(#220),#43976);
#203=STYLED_ITEM('',(#44160),#220);
#220=MANIFOLD_SOLID_BREP('Body1',#11244);
#250=B_SPLINE_SURFACE_WITH_KNOTS('',3,3,((#37705,#37706,#37707,#37708,#37709,
#37710,#37711,#37712,#37713,#37714,#37715,#37716,#37717,#37718,#37719,#37720,
#37721,#37722,#37723,#37724,#37725,#37726,#37727,#37728,#37729,#37730,#37731,
#37732,#37733,#37734,#37735,#37736,#37737,#37738,#37739,#37740,#37741,#37742,
#37743,#37744,#37745,#37746,#37747,#37748,#37749,#37750,#37751,#37752,#37753,
#37754,#37755,#37756,#37757,#37758,#37759,#37760,#37761,#37762,#37763,#37764,
#37765,#37766,#37767,#37768,#37769,#37770,#37771,#37772,#37773,#37774,#37775,
#37776,#37777,#37778,#37779,#37780,#37781,#37782,#37783,#37784,#37785,#37786,
#37787,#37788,#37789,#37790,#37791,#37792,#37793,#37794,#37795,#37796,#37797,
#37798,#37799,#37800,#37801,#37802,#37803,#37804,#37805,#37806,#37807,#37808,
#37809,#37810),(#37811,#37812,#37813,#37814,#37815,#37816,#37817,#37818,
#37819,#37820,#37821,#37822,#37823,#37824,#37825,#37826,#37827,#37828,#37829,
#37830,#37831,#37832,#37833,#37834,#37835,#37836,#37837,#37838,#37839,#37840,
#37841,#37842,#37843,#37844,#37845,#37846,#37847,#37848,#37849,#37850,#37851,
#37852,#37853,#37854,#37855,#37856,#37857,#37858,#37859,#37860,#37861,#37862,
#37863,#37864,#37865,#37866,#37867,#37868,#37869,#37870,#37871,#37872,#37873,
#37874,#37875,#37876,#37877,#37878,#37879,#37880,#37881,#37882,#37883,#37884,
#37885,#37886,#37887,#37888,#37889,#37890,#37891,#37892,#37893,#37894,#37895,
#37896,#37897,#37898,#37899,#37900,#37901,#37902,#37903,#37904,#37905,#37906,
#37907,#37908,#37909,#37910,#37911,#37912,#37913,#37914,#37915,#37916),
(#37917,#37918,#37919,#37920,#37921,#37922,#37923,#37924,#37925,#37926,
#37927,#37928,#37929,#37930,#37931,#37932,#37933,#37934,#37935,#37936,#37937,
#37938,#37939,#37940,#37941,#37942,#37943,#37944,#37945,#37946,#37947,#37948,
#37949,#37950,#37951,#37952,#37953,#37954,#37955,#37956,#37957,#37958,#37959,
#37960,#37961,#37962,#37963,#37964,#37965,#37966,#37967,#37968,#37969,#37970,
#37971,#37972,#37973,#37974,#37975,#37976,#37977,#37978,#37979,#37980,#37981,
#37982,#37983,#37984,#37985,#37986,#37987,#37988,#37989,#37990,#37991,#37992,
#37993,#37994,#37995,#37996,#37997,#37998,#37999,#38000,#38001,#38002,#38003,
#38004,#38005,#38006,#38007,#38008,#38009,#38010,#38011,#38012,#38013,#38014,
#38015,#38016,#38017,#38018,#38019,#38020,#38021,#38022),(#38023,#38024,
#38025,#38026,#38027,#38028,#38029,#38030,#38031,#38032,#38033,#38034,#38035,
#38036,#38037,#38038,#38039,#38040,#38041,#38042,#38043,#38044,#38045,#38046,
#38047,#38048,#38049,#38050,#38051,#38052,#38053,#38054,#38055,#38056,#38057,
#38058,#38059,#38060,#38061,#38062,#38063,#38064,#38065,#38066,#38067,#38068,
#38069,#38070,#38071,#38072,#38073,#38074,#38075,#38076,#38077,#38078,#38079,
#38080,#38081,#38082,#38083,#38084,#38085,#38086,#38087,#38088,#38089,#38090,
#38091,#38092,#38093,#38094,#38095,#38096,#38097,#38098,#38099,#38100,#38101,
#38102,#38103,#38104,#38105,#38106,#38107,#38108,#38109,#38110,#38111,#38112,
#38113,#38114,#38115,#38116,#38117,#38118,#38119,#38120,#38121,#38122,#38123,
#38124,#38125,#38126,#38127,#38128)),.UNSPECIFIED.,.F.,.F.,.F.,(4,4),(4,
1,1,1,1,1,1,1,1,1,1,1,1,1,1,1,1,1,1,1,1,1,1,1,1,1,1,1,1,1,1,1,1,1,1,1,1,
1,1,1,1,1,1,1,1,1,1,1,1,1,1,1,1,1,1,1,1,1,1,1,1,1,1,1,1,1,1,1,1,1,1,1,1,
1,1,1,1,1,1,1,1,1,1,1,1,1,1,1,1,1,1,1,1,1,1,1,1,1,1,1,1,1,1,4),(0.,0.0460148164544132),
(11.6154215191105,12.6127573616628,13.610093204215,14.6074290467673,15.6047648893195,
16.6021007318718,17.599436574424,18.5967724169762,19.5941082595285,20.5914441020807,
21.588779944633,22.5861157871852,23.5834516297375,24.5807874722897,25.5781233148419,
26.5754591573942,27.5727949999464,28.5701308424987,29.5674666850509,30.5648025276032,
31.5621383701554,32.5594742127077,33.5568100552599,34.5541458978121,35.5514817403644,
36.5488175829166,37.5461534254689,38.5434892680211,39.5408251105734,40.5381609531256,
41.5354967956779,42.5328326382301,43.5301684807823,44.5275043233346,45.5248401658868,
46.5221760084391,47.5195118509913,48.5168476935436,49.5141835360958,50.5115193786481,
51.5088552212003,52.5061910637525,53.5035269063048,54.500862748857,55.4981985914093,
56.4955344339615,57.4928702765138,58.490206119066,59.4875419616182,60.4848778041705,
61.4822136467227,62.479549489275,63.4768853318272,64.4742211743795,65.4715570169317,
66.468892859484,67.4662287020362,68.4635645445884,69.4609003871407,70.4582362296929,
71.4555720722452,72.4529079147974,73.4502437573497,74.4475795999019,75.4449154424541,
76.4422512850064,77.4395871275586,78.4369229701109,79.4342588126631,80.4315946552154,
81.4289304977676,82.4262663403199,83.4236021828721,84.4209380254243,85.4182738679766,
86.4156097105288,87.4129455530811,88.4102813956333,89.4076172381856,90.4049530807378,
91.4022889232901,92.3996247658423,93.3969606083945,94.3942964509468,95.391632293499,
96.3889681360513,97.3863039786035,98.3836398211558,99.380975663708,100.37831150626,
101.375647348812,102.372983191365,103.370319033917,104.367654876469,105.364990719021,
106.362326561574,107.359662404126,108.356998246678,109.35433408923,110.351669931783,
111.349005774335,112.346341616887,113.343677459439,114.341013301992),
 .UNSPECIFIED.);
#251=B_SPLINE_SURFACE_WITH_KNOTS('',3,3,((#38221,#38222,#38223,#38224,#38225,
#38226,#38227,#38228,#38229,#38230,#38231,#38232,#38233,#38234,#38235,#38236,
#38237,#38238,#38239,#38240,#38241,#38242,#38243,#38244,#38245,#38246,#38247,
#38248,#38249,#38250,#38251,#38252,#38253,#38254,#38255,#38256,#38257,#38258,
#38259,#38260,#38261,#38262,#38263,#38264,#38265,#38266,#38267,#38268,#38269,
#38270,#38271,#38272,#38273,#38274,#38275,#38276,#38277,#38278,#38279,#38280,
#38281,#38282,#38283,#38284,#38285,#38286,#38287,#38288,#38289,#38290,#38291,
#38292,#38293,#38294,#38295,#38296,#38297,#38298,#38299,#38300,#38301,#38302,
#38303,#38304,#38305,#38306,#38307,#38308,#38309,#38310,#38311,#38312,#38313,
#38314,#38315,#38316,#38317,#38318,#38319,#38320,#38321,#38322,#38323,#38324,
#38325,#38326,#38327,#38328),(#38329,#38330,#38331,#38332,#38333,#38334,
#38335,#38336,#38337,#38338,#38339,#38340,#38341,#38342,#38343,#38344,#38345,
#38346,#38347,#38348,#38349,#38350,#38351,#38352,#38353,#38354,#38355,#38356,
#38357,#38358,#38359,#38360,#38361,#38362,#38363,#38364,#38365,#38366,#38367,
#38368,#38369,#38370,#38371,#38372,#38373,#38374,#38375,#38376,#38377,#38378,
#38379,#38380,#38381,#38382,#38383,#38384,#38385,#38386,#38387,#38388,#38389,
#38390,#38391,#38392,#38393,#38394,#38395,#38396,#38397,#38398,#38399,#38400,
#38401,#38402,#38403,#38404,#38405,#38406,#38407,#38408,#38409,#38410,#38411,
#38412,#38413,#38414,#38415,#38416,#38417,#38418,#38419,#38420,#38421,#38422,
#38423,#38424,#38425,#38426,#38427,#38428,#38429,#38430,#38431,#38432,#38433,
#38434,#38435,#38436),(#38437,#38438,#38439,#38440,#38441,#38442,#38443,
#38444,#38445,#38446,#38447,#38448,#38449,#38450,#38451,#38452,#38453,#38454,
#38455,#38456,#38457,#38458,#38459,#38460,#38461,#38462,#38463,#38464,#38465,
#38466,#38467,#38468,#38469,#38470,#38471,#38472,#38473,#38474,#38475,#38476,
#38477,#38478,#38479,#38480,#38481,#38482,#38483,#38484,#38485,#38486,#38487,
#38488,#38489,#38490,#38491,#38492,#38493,#38494,#38495,#38496,#38497,#38498,
#38499,#38500,#38501,#38502,#38503,#38504,#38505,#38506,#38507,#38508,#38509,
#38510,#38511,#38512,#38513,#38514,#38515,#38516,#38517,#38518,#38519,#38520,
#38521,#38522,#38523,#38524,#38525,#38526,#38527,#38528,#38529,#38530,#38531,
#38532,#38533,#38534,#38535,#38536,#38537,#38538,#38539,#38540,#38541,#38542,
#38543,#38544),(#38545,#38546,#38547,#38548,#38549,#38550,#38551,#38552,
#38553,#38554,#38555,#38556,#38557,#38558,#38559,#38560,#38561,#38562,#38563,
#38564,#38565,#38566,#38567,#38568,#38569,#38570,#38571,#38572,#38573,#38574,
#38575,#38576,#38577,#38578,#38579,#38580,#38581,#38582,#38583,#38584,#38585,
#38586,#38587,#38588,#38589,#38590,#38591,#38592,#38593,#38594,#38595,#38596,
#38597,#38598,#38599,#38600,#38601,#38602,#38603,#38604,#38605,#38606,#38607,
#38608,#38609,#38610,#38611,#38612,#38613,#38614,#38615,#38616,#38617,#38618,
#38619,#38620,#38621,#38622,#38623,#38624,#38625,#38626,#38627,#38628,#38629,
#38630,#38631,#38632,#38633,#38634,#38635,#38636,#38637,#38638,#38639,#38640,
#38641,#38642,#38643,#38644,#38645,#38646,#38647,#38648,#38649,#38650,#38651,
#38652)),.UNSPECIFIED.,.F.,.F.,.F.,(4,4),(4,1,1,1,1,1,1,1,1,1,1,1,1,1,1,
1,1,1,1,1,1,1,1,1,1,1,1,1,1,1,1,1,1,1,1,1,1,1,1,1,1,1,1,1,1,1,1,1,1,1,1,
1,1,1,1,1,1,1,1,1,1,1,1,1,1,1,1,1,1,1,1,1,1,1,1,1,1,1,1,1,1,1,1,1,1,1,1,
1,1,1,1,1,1,1,1,1,1,1,1,1,1,1,1,1,1,4),(0.,0.0460148164544132),(8.31058692273969,
9.30859389336977,10.3066008639999,11.30460783463,12.30261480526,13.3006217758901,
14.2986287465202,15.2966357171503,16.2946426877804,17.2926496584105,18.2906566290406,
19.2886635996707,20.2866705703008,21.2846775409308,22.2826845115609,23.280691482191,
24.2786984528211,25.2767054234512,26.2747123940813,27.2727193647114,28.2707263353415,
29.2687333059716,30.2667402766016,31.2647472472317,32.2627542178618,33.2607611884919,
34.258768159122,35.2567751297521,36.2547821003822,37.2527890710123,38.2507960416424,
39.2488030122724,40.2468099829025,41.2448169535326,42.2428239241627,43.2408308947928,
44.2388378654229,45.236844836053,46.2348518066831,47.2328587773132,48.2308657479432,
49.2288727185733,50.2268796892034,51.2248866598335,52.2228936304636,53.2209006010937,
54.2189075717238,55.2169145423539,56.214921512984,57.212928483614,58.2109354542441,
59.2089424248742,60.2069493955043,61.2049563661344,62.2029633367645,63.2009703073946,
64.1989772780247,65.1969842486548,66.1949912192848,67.1929981899149,68.191005160545,
69.1890121311751,70.1870191018052,71.1850260724353,72.1830330430654,73.1810400136955,
74.1790469843256,75.1770539549557,76.1750609255857,77.1730678962158,78.1710748668459,
79.169081837476,80.1670888081061,81.1650957787362,82.1631027493663,83.1611097199964,
84.1591166906264,85.1571236612565,86.1551306318866,87.1531376025167,88.1511445731468,
89.1491515437769,90.147158514407,91.1451654850371,92.1431724556672,93.1411794262973,
94.1391863969273,95.1371933675574,96.1352003381875,97.1332073088176,98.1312142794477,
99.1292212500778,100.127228220708,101.125235191338,102.123242161968,103.121249132598,
104.119256103228,105.117263073858,106.115270044488,107.113277015118,108.111283985749,
109.109290956379,110.107297927009,111.105304897639,112.103311868269,113.101318838899),
 .UNSPECIFIED.);
#323=FACE_BOUND('',#1682,.T.);
#324=FACE_BOUND('',#1685,.T.);
#444=PLANE('',#12094);
#445=PLANE('',#12095);
#446=PLANE('',#12096);
#447=PLANE('',#12097);
#448=PLANE('',#12098);
#449=PLANE('',#12099);
#450=PLANE('',#12100);
#451=PLANE('',#12101);
#452=PLANE('',#12105);
#453=PLANE('',#12106);
#950=FACE_OUTER_BOUND('',#1637,.T.);
#951=FACE_OUTER_BOUND('',#1638,.T.);
#952=FACE_OUTER_BOUND('',#1639,.T.);
#953=FACE_OUTER_BOUND('',#1640,.T.);
#954=FACE_OUTER_BOUND('',#1641,.T.);
#955=FACE_OUTER_BOUND('',#1642,.T.);
#956=FACE_OUTER_BOUND('',#1643,.T.);
#957=FACE_OUTER_BOUND('',#1644,.T.);
#958=FACE_OUTER_BOUND('',#1645,.T.);
#959=FACE_OUTER_BOUND('',#1646,.T.);
#960=FACE_OUTER_BOUND('',#1647,.T.);
#961=FACE_OUTER_BOUND('',#1648,.T.);
#962=FACE_OUTER_BOUND('',#1649,.T.);
#963=FACE_OUTER_BOUND('',#1650,.T.);
#964=FACE_OUTER_BOUND('',#1651,.T.);
#965=FACE_OUTER_BOUND('',#1652,.T.);
#966=FACE_OUTER_BOUND('',#1653,.T.);
#967=FACE_OUTER_BOUND('',#1654,.T.);
#968=FACE_OUTER_BOUND('',#1655,.T.);
#969=FACE_OUTER_BOUND('',#1656,.T.);
#970=FACE_OUTER_BOUND('',#1657,.T.);
#971=FACE_OUTER_BOUND('',#1658,.T.);
#972=FACE_OUTER_BOUND('',#1659,.T.);
#973=FACE_OUTER_BOUND('',#1660,.T.);
#974=FACE_OUTER_BOUND('',#1661,.T.);
#975=FACE_OUTER_BOUND('',#1662,.T.);
#976=FACE_OUTER_BOUND('',#1663,.T.);
#977=FACE_OUTER_BOUND('',#1664,.T.);
#978=FACE_OUTER_BOUND('',#1665,.T.);
#979=FACE_OUTER_BOUND('',#1666,.T.);
#980=FACE_OUTER_BOUND('',#1667,.T.);
#981=FACE_OUTER_BOUND('',#1668,.T.);
#982=FACE_OUTER_BOUND('',#1669,.T.);
#983=FACE_OUTER_BOUND('',#1670,.T.);
#984=FACE_OUTER_BOUND('',#1671,.T.);
#985=FACE_OUTER_BOUND('',#1672,.T.);
#986=FACE_OUTER_BOUND('',#1673,.T.);
#987=FACE_OUTER_BOUND('',#1674,.T.);
#988=FACE_OUTER_BOUND('',#1675,.T.);
#989=FACE_OUTER_BOUND('',#1676,.T.);
#990=FACE_OUTER_BOUND('',#1677,.T.);
#991=FACE_OUTER_BOUND('',#1678,.T.);
#992=FACE_OUTER_BOUND('',#1679,.T.);
#993=FACE_OUTER_BOUND('',#1680,.T.);
#994=FACE_OUTER_BOUND('',#1681,.T.);
#995=FACE_OUTER_BOUND('',#1683,.T.);
#996=FACE_OUTER_BOUND('',#1684,.T.);
#997=FACE_OUTER_BOUND('',#1686,.T.);
#1637=EDGE_LOOP('',(#9343,#9344,#9345,#9346));
#1638=EDGE_LOOP('',(#9347,#9348,#9349,#9350));
#1639=EDGE_LOOP('',(#9351,#9352,#9353,#9354));
#1640=EDGE_LOOP('',(#9355,#9356,#9357,#9358));
#1641=EDGE_LOOP('',(#9359,#9360,#9361,#9362));
#1642=EDGE_LOOP('',(#9363,#9364,#9365,#9366));
#1643=EDGE_LOOP('',(#9367,#9368,#9369,#9370));
#1644=EDGE_LOOP('',(#9371,#9372,#9373,#9374));
#1645=EDGE_LOOP('',(#9375,#9376,#9377,#9378));
#1646=EDGE_LOOP('',(#9379,#9380,#9381,#9382));
#1647=EDGE_LOOP('',(#9383,#9384,#9385,#9386));
#1648=EDGE_LOOP('',(#9387,#9388,#9389,#9390));
#1649=EDGE_LOOP('',(#9391,#9392,#9393,#9394));
#1650=EDGE_LOOP('',(#9395,#9396,#9397,#9398));
#1651=EDGE_LOOP('',(#9399,#9400,#9401,#9402));
#1652=EDGE_LOOP('',(#9403,#9404,#9405,#9406));
#1653=EDGE_LOOP('',(#9407,#9408,#9409,#9410));
#1654=EDGE_LOOP('',(#9411,#9412,#9413,#9414));
#1655=EDGE_LOOP('',(#9415,#9416,#9417,#9418));
#1656=EDGE_LOOP('',(#9419,#9420,#9421,#9422));
#1657=EDGE_LOOP('',(#9423,#9424,#9425,#9426));
#1658=EDGE_LOOP('',(#9427,#9428,#9429,#9430));
#1659=EDGE_LOOP('',(#9431,#9432,#9433,#9434));
#1660=EDGE_LOOP('',(#9435,#9436,#9437,#9438));
#1661=EDGE_LOOP('',(#9439,#9440,#9441,#9442));
#1662=EDGE_LOOP('',(#9443,#9444,#9445,#9446));
#1663=EDGE_LOOP('',(#9447,#9448,#9449,#9450));
#1664=EDGE_LOOP('',(#9451,#9452,#9453,#9454));
#1665=EDGE_LOOP('',(#9455,#9456,#9457,#9458));
#1666=EDGE_LOOP('',(#9459,#9460,#9461,#9462));
#1667=EDGE_LOOP('',(#9463,#9464,#9465,#9466));
#1668=EDGE_LOOP('',(#9467,#9468,#9469,#9470));
#1669=EDGE_LOOP('',(#9471,#9472,#9473,#9474,#9475,#9476,#9477,#9478));
#1670=EDGE_LOOP('',(#9479,#9480,#9481,#9482,#9483,#9484,#9485,#9486,#9487,
#9488,#9489,#9490,#9491,#9492,#9493,#9494,#9495,#9496,#9497,#9498,#9499,
#9500,#9501,#9502,#9503,#9504,#9505,#9506,#9507,#9508,#9509,#9510,#9511,
#9512,#9513,#9514));
#1671=EDGE_LOOP('',(#9515,#9516,#9517,#9518));
#1672=EDGE_LOOP('',(#9519,#9520,#9521,#9522,#9523,#9524,#9525,#9526,#9527,
#9528,#9529,#9530,#9531,#9532,#9533,#9534,#9535,#9536,#9537,#9538,#9539,
#9540,#9541,#9542,#9543,#9544,#9545,#9546,#9547,#9548,#9549,#9550,#9551,
#9552,#9553,#9554,#9555));
#1673=EDGE_LOOP('',(#9556,#9557,#9558,#9559));
#1674=EDGE_LOOP('',(#9560,#9561,#9562,#9563));
#1675=EDGE_LOOP('',(#9564,#9565,#9566,#9567));
#1676=EDGE_LOOP('',(#9568,#9569,#9570,#9571));
#1677=EDGE_LOOP('',(#9572,#9573,#9574,#9575));
#1678=EDGE_LOOP('',(#9576,#9577,#9578,#9579));
#1679=EDGE_LOOP('',(#9580,#9581,#9582,#9583));
#1680=EDGE_LOOP('',(#9584,#9585,#9586,#9587,#9588,#9589));
#1681=EDGE_LOOP('',(#9590));
#1682=EDGE_LOOP('',(#9591,#9592,#9593,#9594));
#1683=EDGE_LOOP('',(#9595,#9596,#9597,#9598));
#1684=EDGE_LOOP('',(#9599));
#1685=EDGE_LOOP('',(#9600,#9601,#9602,#9603,#9604,#9605));
#1686=EDGE_LOOP('',(#9606));
#1964=CIRCLE('',#12055,0.1954);
#1965=CIRCLE('',#12072,0.15555);
#1966=CIRCLE('',#12089,0.1954);
#1967=CIRCLE('',#12090,0.1);
#1968=CIRCLE('',#12092,0.15555);
#1969=CIRCLE('',#12102,0.35);
#1970=CIRCLE('',#12104,0.35);
#2610=B_SPLINE_CURVE_WITH_KNOTS('',3,(#36376,#36377,#36378,#36379,#36380,
#36381,#36382,#36383,#36384,#36385),.UNSPECIFIED.,.F.,.F.,(4,3,3,4),(-4.09254174883833,
-3.98934337020898,-2.99200752765673,-2.06514013327813),.UNSPECIFIED.);
#2611=B_SPLINE_CURVE_WITH_KNOTS('',3,(#36388,#36389,#36390,#36391,#36392,
#36393,#36394),.UNSPECIFIED.,.F.,.F.,(4,3,4),(0.,0.998006970630082,1.11419103802948),
 .UNSPECIFIED.);
#2612=B_SPLINE_CURVE_WITH_KNOTS('',3,(#36399,#36400,#36401,#36402,#36403,
#36404,#36405,#36406,#36407,#36408,#36409,#36410,#36411,#36412,#36413,#36414,
#36415,#36416,#36417,#36418,#36419,#36420),.UNSPECIFIED.,.F.,.F.,(4,3,3,
3,3,3,3,4),(-10.3757270560179,-9.97335842552244,-8.9760225829702,-7.97868674041795,
-6.9813508978657,-5.98401505531347,-4.98667921276122,-4.09254174883833),
 .UNSPECIFIED.);
#2613=B_SPLINE_CURVE_WITH_KNOTS('',3,(#36421,#36422,#36423,#36424,#36425,
#36426,#36427,#36428,#36429,#36430,#36431,#36432,#36433,#36434,#36435,#36436,
#36437,#36438,#36439,#36440,#36441,#36442),.UNSPECIFIED.,.F.,.F.,(4,3,3,
3,3,3,3,4),(1.11419103802948,1.99601394126018,2.99402091189026,3.99202788252035,
4.99003485315045,5.98804182378054,6.98604879441062,7.39737634520907),
 .UNSPECIFIED.);
#2614=B_SPLINE_CURVE_WITH_KNOTS('',3,(#36447,#36448,#36449,#36450,#36451,
#36452,#36453,#36454,#36455,#36456,#36457,#36458,#36459,#36460,#36461,#36462,
#36463,#36464,#36465,#36466,#36467,#36468),.UNSPECIFIED.,.F.,.F.,(4,3,3,
3,3,3,3,4),(-16.6589123631975,-15.9573734808359,-14.9600376382837,-13.9627017957314,
-12.9653659531792,-11.9680301106269,-10.9706942680747,-10.3757270560179),
 .UNSPECIFIED.);
#2615=B_SPLINE_CURVE_WITH_KNOTS('',3,(#36469,#36470,#36471,#36472,#36473,
#36474,#36475,#36476,#36477,#36478,#36479,#36480,#36481,#36482,#36483,#36484,
#36485,#36486,#36487,#36488,#36489,#36490),.UNSPECIFIED.,.F.,.F.,(4,3,3,
3,3,3,3,4),(7.39737634520907,7.98405576504071,8.9820627356708,9.98006970630089,
10.978076676931,11.9760836475611,12.9740906181912,13.6805616523887),
 .UNSPECIFIED.);
#2616=B_SPLINE_CURVE_WITH_KNOTS('',3,(#36495,#36496,#36497,#36498,#36499,
#36500,#36501,#36502,#36503,#36504,#36505,#36506,#36507,#36508,#36509,#36510,
#36511,#36512,#36513,#36514,#36515,#36516),.UNSPECIFIED.,.F.,.F.,(4,3,3,
3,3,3,3,4),(-22.9420976703771,-21.9413885361494,-20.9440526935971,-19.9467168510449,
-18.9493810084926,-17.9520451659404,-16.9547093233881,-16.6589123631975),
 .UNSPECIFIED.);
#2617=B_SPLINE_CURVE_WITH_KNOTS('',3,(#36517,#36518,#36519,#36520,#36521,
#36522,#36523,#36524,#36525,#36526,#36527,#36528,#36529,#36530,#36531,#36532,
#36533,#36534,#36535,#36536,#36537,#36538),.UNSPECIFIED.,.F.,.F.,(4,3,3,
3,3,3,3,4),(13.6805616523887,13.9720975888212,14.9701045594513,15.9681115300814,
16.9661185007115,17.9641254713416,18.9621324419717,19.9637469595682),
 .UNSPECIFIED.);
#2618=B_SPLINE_CURVE_WITH_KNOTS('',3,(#36543,#36544,#36545,#36546,#36547,
#36548,#36549,#36550,#36551,#36552,#36553,#36554,#36555,#36556,#36557,#36558,
#36559,#36560,#36561,#36562,#36563,#36564),.UNSPECIFIED.,.F.,.F.,(4,3,3,
3,3,3,3,4),(-29.2252829775567,-28.9227394340151,-27.9254035914628,-26.9280677489106,
-25.9307319063583,-24.9333960638061,-23.9360602212539,-22.9420976703771),
 .UNSPECIFIED.);
#2619=B_SPLINE_CURVE_WITH_KNOTS('',3,(#36565,#36566,#36567,#36568,#36569,
#36570,#36571,#36572,#36573,#36574,#36575,#36576,#36577,#36578,#36579,#36580,
#36581,#36582,#36583,#36584,#36585,#36586),.UNSPECIFIED.,.F.,.F.,(4,3,3,
3,3,3,3,4),(19.9637469595682,20.9581463832319,21.956153353862,22.954160324492,
23.9521672951221,24.9501742657522,25.9481812363823,26.2469322667478),
 .UNSPECIFIED.);
#2620=B_SPLINE_CURVE_WITH_KNOTS('',3,(#36591,#36592,#36593,#36594,#36595,
#36596,#36597,#36598,#36599,#36600,#36601,#36602,#36603,#36604,#36605,#36606,
#36607,#36608,#36609,#36610,#36611,#36612),.UNSPECIFIED.,.F.,.F.,(4,3,3,
3,3,3,3,4),(-35.5084682847363,-34.9067544893285,-33.9094186467763,-32.9120828042241,
-31.9147469616718,-30.9174111191196,-29.9200752765673,-29.2252829775567),
 .UNSPECIFIED.);
#2621=B_SPLINE_CURVE_WITH_KNOTS('',3,(#36613,#36614,#36615,#36616,#36617,
#36618,#36619,#36620,#36621,#36622,#36623,#36624,#36625,#36626,#36627,#36628,
#36629,#36630,#36631,#36632,#36633,#36634),.UNSPECIFIED.,.F.,.F.,(4,3,3,
3,3,3,3,4),(26.2469322667478,26.9461882070124,27.9441951776425,28.9422021482726,
29.9402091189027,30.9382160895327,31.9362230601628,32.5301175739274),
 .UNSPECIFIED.);
#2622=B_SPLINE_CURVE_WITH_KNOTS('',3,(#36639,#36640,#36641,#36642,#36643,
#36644,#36645,#36646,#36647,#36648,#36649,#36650,#36651,#36652,#36653,#36654,
#36655,#36656,#36657,#36658,#36659,#36660),.UNSPECIFIED.,.F.,.F.,(4,3,3,
3,3,3,3,4),(-41.7916535919159,-40.890769544642,-39.8934337020898,-38.8960978595375,
-37.8987620169853,-36.901426174433,-35.9040903318808,-35.5084682847363),
 .UNSPECIFIED.);
#2623=B_SPLINE_CURVE_WITH_KNOTS('',3,(#36661,#36662,#36663,#36664,#36665,
#36666,#36667,#36668,#36669,#36670,#36671,#36672,#36673,#36674,#36675,#36676,
#36677,#36678,#36679,#36680,#36681,#36682),.UNSPECIFIED.,.F.,.F.,(4,3,3,
3,3,3,3,4),(32.5301175739274,32.9342300307929,33.932237001423,34.9302439720531,
35.9282509426832,36.9262579133133,37.9242648839434,38.813302881107),
 .UNSPECIFIED.);
#2624=B_SPLINE_CURVE_WITH_KNOTS('',3,(#36687,#36688,#36689,#36690,#36691,
#36692,#36693,#36694,#36695,#36696,#36697,#36698,#36699,#36700,#36701,#36702,
#36703,#36704,#36705,#36706,#36707,#36708,#36709,#36710,#36711),
 .UNSPECIFIED.,.F.,.F.,(4,3,3,3,3,3,3,3,4),(-48.0748388990955,-47.8721204425077,
-46.8747845999555,-45.8774487574032,-44.880112914851,-43.8827770722987,
-42.8854412297465,-41.8881053871943,-41.7916535919159),.UNSPECIFIED.);
#2625=B_SPLINE_CURVE_WITH_KNOTS('',3,(#36712,#36713,#36714,#36715,#36716,
#36717,#36718,#36719,#36720,#36721,#36722,#36723,#36724,#36725,#36726,#36727,
#36728,#36729,#36730,#36731,#36732,#36733,#36734,#36735,#36736),
 .UNSPECIFIED.,.F.,.F.,(4,3,3,3,3,3,3,3,4),(38.813302881107,38.9222718545735,
39.9202788252036,40.9182857958337,41.9162927664637,42.9142997370938,43.9123067077239,
44.910313678354,45.0964881882866),.UNSPECIFIED.);
#2626=B_SPLINE_CURVE_WITH_KNOTS('',3,(#36741,#36742,#36743,#36744,#36745,
#36746,#36747,#36748,#36749,#36750,#36751,#36752,#36753,#36754,#36755,#36756,
#36757,#36758,#36759,#36760,#36761,#36762),.UNSPECIFIED.,.F.,.F.,(4,3,3,
3,3,3,3,4),(-54.3580242062751,-53.8561354978212,-52.8587996552689,-51.8614638127167,
-50.8641279701645,-49.8667921276122,-48.86945628506,-48.0748388990955),
 .UNSPECIFIED.);
#2627=B_SPLINE_CURVE_WITH_KNOTS('',3,(#36763,#36764,#36765,#36766,#36767,
#36768,#36769,#36770,#36771,#36772,#36773,#36774,#36775,#36776,#36777,#36778,
#36779,#36780,#36781,#36782,#36783,#36784),.UNSPECIFIED.,.F.,.F.,(4,3,3,
3,3,3,3,4),(45.0964881882866,45.9083206489841,46.9063276196142,47.9043345902443,
48.9023415608744,49.9003485315045,50.8983555021345,51.3796734954662),
 .UNSPECIFIED.);
#2628=B_SPLINE_CURVE_WITH_KNOTS('',3,(#36789,#36790,#36791,#36792,#36793,
#36794,#36795,#36796,#36797,#36798,#36799,#36800,#36801,#36802,#36803,#36804,
#36805,#36806,#36807,#36808,#36809,#36810),.UNSPECIFIED.,.F.,.F.,(4,3,3,
3,3,3,3,4),(-60.6412095134546,-59.8401505531347,-58.8428147105824,-57.8454788680302,
-56.8481430254779,-55.8508071829257,-54.8534713403734,-54.3580242062751),
 .UNSPECIFIED.);
#2629=B_SPLINE_CURVE_WITH_KNOTS('',3,(#36811,#36812,#36813,#36814,#36815,
#36816,#36817,#36818,#36819,#36820,#36821,#36822,#36823,#36824,#36825,#36826,
#36827,#36828,#36829,#36830,#36831,#36832),.UNSPECIFIED.,.F.,.F.,(4,3,3,
3,3,3,3,4),(51.3796734954662,51.8963624727646,52.8943694433947,53.8923764140248,
54.8903833846549,55.888390355285,56.8863973259151,57.6628588026458),
 .UNSPECIFIED.);
#2630=B_SPLINE_CURVE_WITH_KNOTS('',3,(#36837,#36838,#36839,#36840,#36841,
#36842,#36843,#36844,#36845,#36846,#36847,#36848,#36849,#36850,#36851,#36852,
#36853,#36854,#36855,#36856,#36857,#36858,#36859,#36860,#36861),
 .UNSPECIFIED.,.F.,.F.,(4,3,3,3,3,3,3,3,4),(-66.9243948206342,-66.8215014510004,
-65.8241656084481,-64.8268297658959,-63.8294939233436,-62.8321580807914,
-61.8348222382391,-60.8374863956869,-60.6412095134546),.UNSPECIFIED.);
#2631=B_SPLINE_CURVE_WITH_KNOTS('',3,(#36862,#36863,#36864,#36865,#36866,
#36867,#36868,#36869,#36870,#36871,#36872,#36873,#36874,#36875,#36876,#36877,
#36878,#36879,#36880,#36881,#36882,#36883,#36884,#36885,#36886),
 .UNSPECIFIED.,.F.,.F.,(4,3,3,3,3,3,3,3,4),(57.6628588026458,57.8844042965452,
58.8824112671752,59.8804182378054,60.8784252084354,61.8764321790655,62.8744391496956,
63.8724461203257,63.9460441098254),.UNSPECIFIED.);
#2632=B_SPLINE_CURVE_WITH_KNOTS('',3,(#36891,#36892,#36893,#36894,#36895,
#36896,#36897,#36898,#36899,#36900,#36901,#36902,#36903,#36904,#36905,#36906,
#36907,#36908,#36909,#36910,#36911,#36912),.UNSPECIFIED.,.F.,.F.,(4,3,3,
3,3,3,3,4),(-73.2075801278138,-72.8055165063138,-71.8081806637616,-70.8108448212093,
-69.8135089786571,-68.8161731361048,-67.8188372935526,-66.9243948206342),
 .UNSPECIFIED.);
#2633=B_SPLINE_CURVE_WITH_KNOTS('',3,(#36913,#36914,#36915,#36916,#36917,
#36918,#36919,#36920,#36921,#36922,#36923,#36924,#36925,#36926,#36927,#36928,
#36929,#36930,#36931,#36932,#36933,#36934),.UNSPECIFIED.,.F.,.F.,(4,3,3,
3,3,3,3,4),(63.9460441098254,64.8704530909558,65.8684600615859,66.866467032216,
67.8644740028461,68.8624809734761,69.8604879441062,70.229229417005),
 .UNSPECIFIED.);
#2634=B_SPLINE_CURVE_WITH_KNOTS('',3,(#36939,#36940,#36941,#36942,#36943,
#36944,#36945,#36946,#36947,#36948,#36949,#36950,#36951,#36952,#36953,#36954,
#36955,#36956,#36957,#36958,#36959,#36960),.UNSPECIFIED.,.F.,.F.,(4,3,3,
3,3,3,3,4),(-79.4907654349934,-78.7895315616273,-77.792195719075,-76.7948598765228,
-75.7975240339705,-74.8001881914183,-73.802852348866,-73.2075801278138),
 .UNSPECIFIED.);
#2635=B_SPLINE_CURVE_WITH_KNOTS('',3,(#36961,#36962,#36963,#36964,#36965,
#36966,#36967,#36968,#36969,#36970,#36971,#36972,#36973,#36974,#36975,#36976,
#36977,#36978,#36979,#36980,#36981,#36982),.UNSPECIFIED.,.F.,.F.,(4,3,3,
3,3,3,3,4),(70.229229417005,70.8584949147363,71.8565018853664,72.8545088559965,
73.8525158266266,74.8505227972567,75.8485297678868,76.5124147241846),
 .UNSPECIFIED.);
#2636=B_SPLINE_CURVE_WITH_KNOTS('',3,(#36987,#36988,#36989,#36990,#36991,
#36992,#36993,#36994,#36995,#36996,#36997,#36998,#36999,#37000,#37001,#37002,
#37003,#37004,#37005,#37006,#37007,#37008),.UNSPECIFIED.,.F.,.F.,(4,3,3,
3,3,3,3,4),(-85.773950742173,-84.7735466169407,-83.7762107743885,-82.7788749318363,
-81.781539089284,-80.7842032467318,-79.7868674041795,-79.4907654349934),
 .UNSPECIFIED.);
#2637=B_SPLINE_CURVE_WITH_KNOTS('',3,(#37009,#37010,#37011,#37012,#37013,
#37014,#37015,#37016,#37017,#37018,#37019,#37020,#37021,#37022,#37023,#37024,
#37025,#37026,#37027,#37028,#37029,#37030),.UNSPECIFIED.,.F.,.F.,(4,3,3,
3,3,3,3,4),(76.5124147241846,76.8465367385169,77.8445437091469,78.842550679777,
79.8405576504071,80.8385646210372,81.8365715916673,82.7956000313642),
 .UNSPECIFIED.);
#2638=B_SPLINE_CURVE_WITH_KNOTS('',3,(#37035,#37036,#37037,#37038,#37039,
#37040,#37041,#37042,#37043,#37044,#37045,#37046,#37047,#37048,#37049,#37050,
#37051,#37052,#37053,#37054,#37055,#37056),.UNSPECIFIED.,.F.,.F.,(4,3,3,
3,3,3,3,4),(-92.0571360493526,-91.7548975148065,-90.7575616722542,-89.760225829702,
-88.7628899871497,-87.7655541445975,-86.7682183020452,-85.773950742173),
 .UNSPECIFIED.);
#2639=B_SPLINE_CURVE_WITH_KNOTS('',3,(#37057,#37058,#37059,#37060,#37061,
#37062,#37063,#37064,#37065,#37066,#37067,#37068,#37069,#37070,#37071,#37072,
#37073,#37074,#37075,#37076,#37077,#37078,#37079,#37080,#37081),
 .UNSPECIFIED.,.F.,.F.,(4,3,3,3,3,3,3,3,4),(82.7956000313642,82.8345785622974,
83.8325855329275,84.8305925035576,85.8285994741877,86.8266064448178,87.8246134154479,
88.822620386078,89.0787853385438),.UNSPECIFIED.);
#2640=B_SPLINE_CURVE_WITH_KNOTS('',3,(#37086,#37087,#37088,#37089,#37090,
#37091,#37092,#37093,#37094,#37095,#37096,#37097,#37098,#37099,#37100,#37101,
#37102,#37103,#37104,#37105,#37106,#37107),.UNSPECIFIED.,.F.,.F.,(4,3,3,
3,3,3,3,4),(-98.3403213565322,-97.7389125701199,-96.7415767275677,-95.7442408850154,
-94.7469050424632,-93.7495691999109,-92.7522333573587,-92.0571360493526),
 .UNSPECIFIED.);
#2641=B_SPLINE_CURVE_WITH_KNOTS('',3,(#37108,#37109,#37110,#37111,#37112,
#37113,#37114,#37115,#37116,#37117,#37118,#37119,#37120,#37121,#37122,#37123,
#37124,#37125,#37126,#37127,#37128,#37129),.UNSPECIFIED.,.F.,.F.,(4,3,3,
3,3,3,3,4),(89.0787853385438,89.820627356708,90.8186343273381,91.8166412979682,
92.8146482685983,93.8126552392284,94.8106622098585,95.3619706457233),
 .UNSPECIFIED.);
#2642=B_SPLINE_CURVE_WITH_KNOTS('',3,(#37135,#37136,#37137,#37138,#37139,
#37140,#37141,#37142),.UNSPECIFIED.,.F.,.F.,(4,1,1,1,1,4),(109.955742875643,
110.351669931783,111.349005774335,112.346341616887,113.343677459439,114.341013301992),
 .UNSPECIFIED.);
#2643=B_SPLINE_CURVE_WITH_KNOTS('',3,(#37145,#37146,#37147,#37148,#37149,
#37150,#37151),.UNSPECIFIED.,.F.,.F.,(4,1,1,1,4),(109.955742875643,110.107297927009,
111.105304897639,112.103311868269,113.101318838899),.UNSPECIFIED.);
#2644=B_SPLINE_CURVE_WITH_KNOTS('',3,(#37156,#37157,#37158,#37159,#37160,
#37161,#37162,#37163,#37164,#37165),.UNSPECIFIED.,.F.,.F.,(4,1,1,1,1,1,
1,4),(103.672557568463,104.367654876469,105.364990719021,106.362326561574,
107.359662404126,108.356998246678,109.35433408923,109.955742875643),
 .UNSPECIFIED.);
#2645=B_SPLINE_CURVE_WITH_KNOTS('',3,(#37166,#37167,#37168,#37169,#37170,
#37171,#37172,#37173,#37174,#37175),.UNSPECIFIED.,.F.,.F.,(4,1,1,1,1,1,
1,4),(103.672557568463,104.119256103228,105.117263073858,106.115270044488,
107.113277015118,108.111283985749,109.109290956379,109.955742875643),
 .UNSPECIFIED.);
#2646=B_SPLINE_CURVE_WITH_KNOTS('',3,(#37180,#37181,#37182,#37183,#37184,
#37185,#37186,#37187,#37188,#37189),.UNSPECIFIED.,.F.,.F.,(4,1,1,1,1,1,
1,4),(97.3893722612836,98.3836398211558,99.380975663708,100.37831150626,
101.375647348812,102.372983191365,103.370319033917,103.672557568463),
 .UNSPECIFIED.);
#2647=B_SPLINE_CURVE_WITH_KNOTS('',3,(#37190,#37191,#37192,#37193,#37194,
#37195,#37196,#37197,#37198,#37199),.UNSPECIFIED.,.F.,.F.,(4,1,1,1,1,1,
1,4),(97.3893722612836,98.1312142794477,99.1292212500778,100.127228220708,
101.125235191338,102.123242161968,103.121249132598,103.672557568463),
 .UNSPECIFIED.);
#2648=B_SPLINE_CURVE_WITH_KNOTS('',3,(#37204,#37205,#37206,#37207,#37208,
#37209,#37210,#37211,#37212,#37213,#37214),.UNSPECIFIED.,.F.,.F.,(4,1,1,
1,1,1,1,1,4),(91.106186954104,91.4022889232901,92.3996247658423,93.3969606083945,
94.3942964509468,95.391632293499,96.3889681360513,97.3863039786035,97.3893722612836),
 .UNSPECIFIED.);
#2649=B_SPLINE_CURVE_WITH_KNOTS('',3,(#37215,#37216,#37217,#37218,#37219,
#37220,#37221,#37222,#37223,#37224,#37225),.UNSPECIFIED.,.F.,.F.,(4,1,1,
1,1,1,1,1,4),(91.106186954104,91.1451654850371,92.1431724556672,93.1411794262973,
94.1391863969273,95.1371933675574,96.1352003381875,97.1332073088176,97.3893722612836),
 .UNSPECIFIED.);
#2650=B_SPLINE_CURVE_WITH_KNOTS('',3,(#37230,#37231,#37232,#37233,#37234,
#37235,#37236,#37237,#37238,#37239),.UNSPECIFIED.,.F.,.F.,(4,1,1,1,1,1,
1,4),(84.8230016469244,85.4182738679766,86.4156097105288,87.4129455530811,
88.4102813956333,89.4076172381856,90.4049530807378,91.106186954104),
 .UNSPECIFIED.);
#2651=B_SPLINE_CURVE_WITH_KNOTS('',3,(#37240,#37241,#37242,#37243,#37244,
#37245,#37246,#37247,#37248,#37249),.UNSPECIFIED.,.F.,.F.,(4,1,1,1,1,1,
1,4),(84.8230016469244,85.1571236612565,86.1551306318866,87.1531376025167,
88.1511445731468,89.1491515437769,90.147158514407,91.106186954104),
 .UNSPECIFIED.);
#2652=B_SPLINE_CURVE_WITH_KNOTS('',3,(#37254,#37255,#37256,#37257,#37258,
#37259,#37260,#37261,#37262,#37263),.UNSPECIFIED.,.F.,.F.,(4,1,1,1,1,1,
1,4),(78.5398163397448,79.4342588126631,80.4315946552154,81.4289304977676,
82.4262663403199,83.4236021828721,84.4209380254243,84.8230016469244),
 .UNSPECIFIED.);
#2653=B_SPLINE_CURVE_WITH_KNOTS('',3,(#37264,#37265,#37266,#37267,#37268,
#37269,#37270,#37271,#37272,#37273),.UNSPECIFIED.,.F.,.F.,(4,1,1,1,1,1,
1,4),(78.5398163397448,79.169081837476,80.1670888081061,81.1650957787362,
82.1631027493663,83.1611097199964,84.1591166906264,84.8230016469244),
 .UNSPECIFIED.);
#2654=B_SPLINE_CURVE_WITH_KNOTS('',3,(#37278,#37279,#37280,#37281,#37282,
#37283,#37284,#37285,#37286,#37287,#37288),.UNSPECIFIED.,.F.,.F.,(4,1,1,
1,1,1,1,1,4),(72.2566310325652,72.4529079147974,73.4502437573497,74.4475795999019,
75.4449154424541,76.4422512850064,77.4395871275586,78.4369229701109,78.5398163397448),
 .UNSPECIFIED.);
#2655=B_SPLINE_CURVE_WITH_KNOTS('',3,(#37289,#37290,#37291,#37292,#37293,
#37294,#37295,#37296,#37297,#37298),.UNSPECIFIED.,.F.,.F.,(4,1,1,1,1,1,
1,4),(72.2566310325652,73.1810400136955,74.1790469843256,75.1770539549557,
76.1750609255857,77.1730678962158,78.1710748668459,78.5398163397448),
 .UNSPECIFIED.);
#2656=B_SPLINE_CURVE_WITH_KNOTS('',3,(#37303,#37304,#37305,#37306,#37307,
#37308,#37309,#37310,#37311,#37312),.UNSPECIFIED.,.F.,.F.,(4,1,1,1,1,1,
1,4),(65.9734457253856,66.468892859484,67.4662287020362,68.4635645445884,
69.4609003871407,70.4582362296929,71.4555720722452,72.2566310325652),
 .UNSPECIFIED.);
#2657=B_SPLINE_CURVE_WITH_KNOTS('',3,(#37313,#37314,#37315,#37316,#37317,
#37318,#37319,#37320,#37321,#37322,#37323),.UNSPECIFIED.,.F.,.F.,(4,1,1,
1,1,1,1,1,4),(65.9734457253856,66.1949912192848,67.1929981899149,68.191005160545,
69.1890121311751,70.1870191018052,71.1850260724353,72.1830330430654,72.2566310325652),
 .UNSPECIFIED.);
#2658=B_SPLINE_CURVE_WITH_KNOTS('',3,(#37328,#37329,#37330,#37331,#37332,
#37333,#37334,#37335,#37336,#37337),.UNSPECIFIED.,.F.,.F.,(4,1,1,1,1,1,
1,4),(59.690260418206,60.4848778041705,61.4822136467227,62.479549489275,
63.4768853318272,64.4742211743795,65.4715570169317,65.9734457253856),
 .UNSPECIFIED.);
#2659=B_SPLINE_CURVE_WITH_KNOTS('',3,(#37338,#37339,#37340,#37341,#37342,
#37343,#37344,#37345,#37346,#37347),.UNSPECIFIED.,.F.,.F.,(4,1,1,1,1,1,
1,4),(59.690260418206,60.2069493955043,61.2049563661344,62.2029633367645,
63.2009703073946,64.1989772780247,65.1969842486548,65.9734457253856),
 .UNSPECIFIED.);
#2660=B_SPLINE_CURVE_WITH_KNOTS('',3,(#37352,#37353,#37354,#37355,#37356,
#37357,#37358,#37359,#37360,#37361,#37362),.UNSPECIFIED.,.F.,.F.,(4,1,1,
1,1,1,1,1,4),(53.4070751110265,53.5035269063048,54.500862748857,55.4981985914093,
56.4955344339615,57.4928702765138,58.490206119066,59.4875419616182,59.690260418206),
 .UNSPECIFIED.);
#2661=B_SPLINE_CURVE_WITH_KNOTS('',3,(#37363,#37364,#37365,#37366,#37367,
#37368,#37369,#37370,#37371,#37372),.UNSPECIFIED.,.F.,.F.,(4,1,1,1,1,1,
1,4),(53.4070751110264,54.2189075717238,55.2169145423539,56.214921512984,
57.212928483614,58.2109354542441,59.2089424248742,59.690260418206),
 .UNSPECIFIED.);
#2662=B_SPLINE_CURVE_WITH_KNOTS('',3,(#37377,#37378,#37379,#37380,#37381,
#37382,#37383,#37384,#37385,#37386),.UNSPECIFIED.,.F.,.F.,(4,1,1,1,1,1,
1,4),(47.1238898038469,47.5195118509913,48.5168476935436,49.5141835360958,
50.5115193786481,51.5088552212003,52.5061910637525,53.4070751110265),
 .UNSPECIFIED.);
#2663=B_SPLINE_CURVE_WITH_KNOTS('',3,(#37387,#37388,#37389,#37390,#37391,
#37392,#37393,#37394,#37395,#37396,#37397),.UNSPECIFIED.,.F.,.F.,(4,1,1,
1,1,1,1,1,4),(47.1238898038468,47.2328587773132,48.2308657479432,49.2288727185733,
50.2268796892034,51.2248866598335,52.2228936304636,53.2209006010937,53.4070751110264),
 .UNSPECIFIED.);
#2664=B_SPLINE_CURVE_WITH_KNOTS('',3,(#37402,#37403,#37404,#37405,#37406,
#37407,#37408,#37409,#37410,#37411),.UNSPECIFIED.,.F.,.F.,(4,1,1,1,1,1,
1,4),(40.8407044966673,41.5354967956779,42.5328326382301,43.5301684807823,
44.5275043233346,45.5248401658868,46.5221760084391,47.1238898038469),
 .UNSPECIFIED.);
#2665=B_SPLINE_CURVE_WITH_KNOTS('',3,(#37412,#37413,#37414,#37415,#37416,
#37417,#37418,#37419,#37420,#37421),.UNSPECIFIED.,.F.,.F.,(4,1,1,1,1,1,
1,4),(40.8407044966672,41.2448169535326,42.2428239241627,43.2408308947928,
44.2388378654229,45.236844836053,46.2348518066831,47.1238898038468),
 .UNSPECIFIED.);
#2666=B_SPLINE_CURVE_WITH_KNOTS('',3,(#37426,#37427,#37428,#37429,#37430,
#37431,#37432,#37433,#37434,#37435),.UNSPECIFIED.,.F.,.F.,(4,1,1,1,1,1,
1,4),(34.5575191894877,35.5514817403644,36.5488175829166,37.5461534254689,
38.5434892680211,39.5408251105734,40.5381609531256,40.8407044966673),
 .UNSPECIFIED.);
#2667=B_SPLINE_CURVE_WITH_KNOTS('',3,(#37436,#37437,#37438,#37439,#37440,
#37441,#37442,#37443,#37444,#37445),.UNSPECIFIED.,.F.,.F.,(4,1,1,1,1,1,
1,4),(34.5575191894876,35.2567751297521,36.2547821003822,37.2527890710123,
38.2507960416424,39.2488030122724,40.2468099829025,40.8407044966672),
 .UNSPECIFIED.);
#2668=B_SPLINE_CURVE_WITH_KNOTS('',3,(#37450,#37451,#37452,#37453,#37454,
#37455,#37456,#37457,#37458,#37459,#37460),.UNSPECIFIED.,.F.,.F.,(4,1,1,
1,1,1,1,1,4),(28.2743338823081,28.5701308424987,29.5674666850509,30.5648025276032,
31.5621383701554,32.5594742127077,33.5568100552599,34.5541458978121,34.5575191894877),
 .UNSPECIFIED.);
#2669=B_SPLINE_CURVE_WITH_KNOTS('',3,(#37461,#37462,#37463,#37464,#37465,
#37466,#37467,#37468,#37469,#37470),.UNSPECIFIED.,.F.,.F.,(4,1,1,1,1,1,
1,4),(28.274333882308,29.2687333059716,30.2667402766016,31.2647472472317,
32.2627542178618,33.2607611884919,34.258768159122,34.5575191894876),
 .UNSPECIFIED.);
#2670=B_SPLINE_CURVE_WITH_KNOTS('',3,(#37475,#37476,#37477,#37478,#37479,
#37480,#37481,#37482,#37483,#37484),.UNSPECIFIED.,.F.,.F.,(4,1,1,1,1,1,
1,4),(21.9911485751285,22.5861157871852,23.5834516297375,24.5807874722897,
25.5781233148419,26.5754591573942,27.5727949999464,28.2743338823081),
 .UNSPECIFIED.);
#2671=B_SPLINE_CURVE_WITH_KNOTS('',3,(#37485,#37486,#37487,#37488,#37489,
#37490,#37491,#37492,#37493,#37494,#37495),.UNSPECIFIED.,.F.,.F.,(4,1,1,
1,1,1,1,1,4),(21.9911485751285,22.2826845115609,23.280691482191,24.2786984528211,
25.2767054234512,26.2747123940813,27.2727193647114,28.2707263353415,28.274333882308),
 .UNSPECIFIED.);
#2672=B_SPLINE_CURVE_WITH_KNOTS('',3,(#37500,#37501,#37502,#37503,#37504,
#37505,#37506,#37507,#37508,#37509),.UNSPECIFIED.,.F.,.F.,(4,1,1,1,1,1,
1,4),(15.7079632679489,16.6021007318718,17.599436574424,18.5967724169762,
19.5941082595285,20.5914441020807,21.588779944633,21.9911485751285),
 .UNSPECIFIED.);
#2673=B_SPLINE_CURVE_WITH_KNOTS('',3,(#37510,#37511,#37512,#37513,#37514,
#37515,#37516,#37517,#37518,#37519),.UNSPECIFIED.,.F.,.F.,(4,1,1,1,1,1,
1,4),(15.7079632679489,16.2946426877804,17.2926496584105,18.2906566290406,
19.2886635996707,20.2866705703008,21.2846775409308,21.9911485751285),
 .UNSPECIFIED.);
#2674=B_SPLINE_CURVE_WITH_KNOTS('',3,(#37522,#37523,#37524,#37525,#37526,
#37527,#37528,#37529,#37530,#37531,#37532,#37533,#37534,#37535,#37536,#37537,
#37538,#37539,#37540,#37541,#37542,#37543,#37544,#37545,#37546,#37547,#37548,
#37549,#37550,#37551,#37552,#37553,#37554,#37555,#37556,#37557,#37558,#37559,
#37560,#37561,#37562,#37563,#37564,#37565,#37566,#37567,#37568,#37569,#37570,
#37571,#37572,#37573,#37574,#37575,#37576,#37577,#37578,#37579,#37580,#37581,
#37582,#37583,#37584,#37585,#37586,#37587,#37588,#37589,#37590,#37591,#37592,
#37593,#37594,#37595,#37596,#37597,#37598,#37599,#37600),.UNSPECIFIED.,
 .F.,.F.,(4,3,3,3,3,3,3,3,3,3,3,3,3,3,3,3,3,3,3,3,3,3,3,3,3,3,4),(-0.996917990983956,
-0.964197655296454,-0.951513094737375,-0.939590005196496,-0.910398139253692,
-0.896458168447615,-0.866624051431682,-0.848513043381918,-0.839276821658768,
-0.836789934415749,-0.803176729602168,-0.780362864215826,-0.769651322799483,
-0.734439153414668,-0.711686399207869,-0.700944767019061,-0.669566542377212,
-0.648981044332524,-0.637888877288902,-0.602287825523676,-0.584615028650125,
-0.570052223933311,-0.532768447080654,-0.516116381189141,-0.50154558318824,
-0.495484670227998,-0.468408511919796),.UNSPECIFIED.);
#2675=B_SPLINE_CURVE_WITH_KNOTS('',3,(#37602,#37603,#37604,#37605,#37606,
#37607,#37608,#37609,#37610,#37611,#37612,#37613,#37614,#37615,#37616,#37617,
#37618,#37619,#37620,#37621,#37622,#37623,#37624,#37625,#37626,#37627,#37628,
#37629,#37630,#37631,#37632,#37633,#37634,#37635),.UNSPECIFIED.,.F.,.F.,
(4,3,3,3,3,3,3,3,3,3,3,4),(-0.271362855059921,-0.23333358174471,-0.202109628804149,
-0.191194824123734,-0.172574372312687,-0.139871461148431,-0.130049418747569,
-0.0948265930323134,-0.0669749700089491,-0.0565955729248257,-0.0239539643597006,
0.),.UNSPECIFIED.);
#2676=B_SPLINE_CURVE_WITH_KNOTS('',3,(#37638,#37639,#37640,#37641,#37642,
#37643,#37644,#37645,#37646,#37647,#37648,#37649,#37650,#37651,#37652,#37653,
#37654,#37655,#37656,#37657,#37658,#37659,#37660,#37661,#37662,#37663,#37664,
#37665,#37666,#37667,#37668,#37669,#37670,#37671,#37672,#37673,#37674,#37675,
#37676,#37677,#37678,#37679,#37680,#37681,#37682,#37683,#37684,#37685,#37686,
#37687,#37688,#37689,#37690,#37691,#37692,#37693,#37694,#37695,#37696,#37697,
#37698,#37699,#37700,#37701),.UNSPECIFIED.,.F.,.F.,(4,3,3,3,3,3,3,3,3,3,
3,3,3,3,3,3,3,3,3,3,3,4),(-0.468408511919796,-0.44532089356327,-0.431869826400524,
-0.394574417707956,-0.377959024336246,-0.36718387876206,-0.329707820210052,
-0.314417154781481,-0.297766482794163,-0.286364248592707,-0.248901620010442,
-0.233074500624702,-0.216543640108336,-0.17799293612575,-0.152182016671258,
-0.141011423916894,-0.12652726456846,-0.094895448426345,-0.0796457512037788,
-0.0683009962329189,-0.0289678476755453,0.),.UNSPECIFIED.);
#2677=B_SPLINE_CURVE_WITH_KNOTS('',3,(#38130,#38131,#38132,#38133,#38134,
#38135,#38136,#38137),.UNSPECIFIED.,.F.,.F.,(4,1,1,1,1,4),(11.6154215191105,
12.6127573616628,13.610093204215,14.6074290467673,15.6047648893195,15.7079632679489),
 .UNSPECIFIED.);
#2678=B_SPLINE_CURVE_WITH_KNOTS('',3,(#38138,#38139,#38140,#38141,#38142,
#38143,#38144,#38145,#38146,#38147,#38148,#38149,#38150,#38151,#38152,#38153,
#38154,#38155,#38156,#38157,#38158,#38159,#38160,#38161,#38162,#38163,#38164,
#38165,#38166,#38167,#38168,#38169,#38170,#38171,#38172,#38173,#38174,#38175,
#38176,#38177,#38178,#38179,#38180,#38181,#38182,#38183,#38184,#38185,#38186,
#38187,#38188,#38189,#38190,#38191,#38192,#38193,#38194,#38195),
 .UNSPECIFIED.,.F.,.F.,(4,3,3,3,3,3,3,3,3,3,3,3,3,3,3,3,3,3,3,4),(-0.364629307890661,
-0.350885759085945,-0.324346713718219,-0.304152838893849,-0.282934787914253,
-0.264003466919189,-0.252764227803326,-0.216347623970161,-0.198031500011342,
-0.186602740018901,-0.166173598315468,-0.146000730648533,-0.128382123165429,
-0.119003916100956,-0.0892529370757172,-0.0724905256163614,-0.0619084956994276,
-0.0517443199161659,-0.0194955210690912,0.),.UNSPECIFIED.);
#2679=B_SPLINE_CURVE_WITH_KNOTS('',3,(#38196,#38197,#38198,#38199,#38200,
#38201,#38202,#38203,#38204,#38205,#38206,#38207,#38208),.UNSPECIFIED.,
 .F.,.F.,(4,3,3,3,4),(-101.213804280572,-100.730920097777,-99.7335842552244,
-98.7362484126722,-98.3403213565322),.UNSPECIFIED.);
#2680=B_SPLINE_CURVE_WITH_KNOTS('',3,(#38211,#38212,#38213,#38214,#38215,
#38216,#38217,#38218,#38219),.UNSPECIFIED.,.F.,.F.,(4,1,1,1,1,1,4),(10.3757270560178,
11.30460783463,12.30261480526,13.3006217758901,14.2986287465202,15.2966357171503,
15.7079632679489),.UNSPECIFIED.);
#2681=B_SPLINE_CURVE_WITH_KNOTS('',3,(#38653,#38654,#38655,#38656,#38657,
#38658,#38659,#38660,#38661,#38662,#38663,#38664,#38665,#38666,#38667,#38668),
 .UNSPECIFIED.,.F.,.F.,(4,3,3,3,3,4),(95.3619706457233,95.8086691804886,
96.8066761511186,97.8046831217487,98.8026900923788,99.1486641472938),
 .UNSPECIFIED.);
#2682=B_SPLINE_CURVE_WITH_KNOTS('',3,(#38669,#38670,#38671,#38672,#38673,
#38674,#38675,#38676,#38677,#38678,#38679,#38680,#38681,#38682,#38683,#38684,
#38685,#38686,#38687,#38688,#38689,#38690,#38691,#38692,#38693,#38694,#38695,
#38696,#38697,#38698,#38699,#38700,#38701,#38702,#38703,#38704,#38705,#38706,
#38707,#38708,#38709,#38710,#38711,#38712,#38713,#38714,#38715,#38716,#38717,
#38718,#38719,#38720),.UNSPECIFIED.,.F.,.F.,(4,3,3,3,3,3,3,3,3,3,3,3,3,
3,3,3,3,4),(-0.366397579005845,-0.355461226466819,-0.328804438442731,-0.31606471842091,
-0.292558951597566,-0.280250898914551,-0.245275213061006,-0.218626183485931,
-0.207947804736759,-0.187209422476688,-0.163808244667102,-0.149577787474042,
-0.13876424622794,-0.104073184670955,-0.0827908372522071,-0.0667764467402658,
-0.0282827470320728,0.),.UNSPECIFIED.);
#3290=LINE('',#36374,#3922);
#3291=LINE('',#36398,#3923);
#3292=LINE('',#36446,#3924);
#3293=LINE('',#36494,#3925);
#3294=LINE('',#36542,#3926);
#3295=LINE('',#36590,#3927);
#3296=LINE('',#36638,#3928);
#3297=LINE('',#36686,#3929);
#3298=LINE('',#36740,#3930);
#3299=LINE('',#36788,#3931);
#3300=LINE('',#36836,#3932);
#3301=LINE('',#36890,#3933);
#3302=LINE('',#36938,#3934);
#3303=LINE('',#36986,#3935);
#3304=LINE('',#37034,#3936);
#3305=LINE('',#37085,#3937);
#3306=LINE('',#37133,#3938);
#3307=LINE('',#37155,#3939);
#3308=LINE('',#37179,#3940);
#3309=LINE('',#37203,#3941);
#3310=LINE('',#37229,#3942);
#3311=LINE('',#37253,#3943);
#3312=LINE('',#37277,#3944);
#3313=LINE('',#37302,#3945);
#3314=LINE('',#37327,#3946);
#3315=LINE('',#37351,#3947);
#3316=LINE('',#37376,#3948);
#3317=LINE('',#37401,#3949);
#3318=LINE('',#37425,#3950);
#3319=LINE('',#37449,#3951);
#3320=LINE('',#37474,#3952);
#3321=LINE('',#37499,#3953);
#3322=LINE('',#37703,#3954);
#3323=LINE('',#38725,#3955);
#3324=LINE('',#38727,#3956);
#3325=LINE('',#38729,#3957);
#3326=LINE('',#38730,#3958);
#3327=LINE('',#38733,#3959);
#3328=LINE('',#38735,#3960);
#3329=LINE('',#38736,#3961);
#3330=LINE('',#38739,#3962);
#3331=LINE('',#38741,#3963);
#3332=LINE('',#38742,#3964);
#3333=LINE('',#38745,#3965);
#3334=LINE('',#38747,#3966);
#3335=LINE('',#38748,#3967);
#3336=LINE('',#38751,#3968);
#3337=LINE('',#38753,#3969);
#3338=LINE('',#38754,#3970);
#3339=LINE('',#38756,#3971);
#3340=LINE('',#38757,#3972);
#3341=LINE('',#38764,#3973);
#3922=VECTOR('',#13965,0.2);
#3923=VECTOR('',#13970,0.2);
#3924=VECTOR('',#13973,0.2);
#3925=VECTOR('',#13976,0.2);
#3926=VECTOR('',#13979,0.2);
#3927=VECTOR('',#13982,0.2);
#3928=VECTOR('',#13985,0.2);
#3929=VECTOR('',#13988,0.2);
#3930=VECTOR('',#13991,0.2);
#3931=VECTOR('',#13994,0.2);
#3932=VECTOR('',#13997,0.2);
#3933=VECTOR('',#14000,0.2);
#3934=VECTOR('',#14003,0.2);
#3935=VECTOR('',#14006,0.2);
#3936=VECTOR('',#14009,0.2);
#3937=VECTOR('',#14012,0.2);
#3938=VECTOR('',#14015,0.15555);
#3939=VECTOR('',#14020,0.15555);
#3940=VECTOR('',#14023,0.15555);
#3941=VECTOR('',#14026,0.15555);
#3942=VECTOR('',#14029,0.15555);
#3943=VECTOR('',#14032,0.15555);
#3944=VECTOR('',#14035,0.15555);
#3945=VECTOR('',#14038,0.15555);
#3946=VECTOR('',#14041,0.15555);
#3947=VECTOR('',#14044,0.15555);
#3948=VECTOR('',#14047,0.15555);
#3949=VECTOR('',#14050,0.15555);
#3950=VECTOR('',#14053,0.15555);
#3951=VECTOR('',#14056,0.15555);
#3952=VECTOR('',#14059,0.15555);
#3953=VECTOR('',#14062,0.15555);
#3954=VECTOR('',#14067,0.15);
#3955=VECTOR('',#14078,1.);
#3956=VECTOR('',#14079,1.);
#3957=VECTOR('',#14080,1.);
#3958=VECTOR('',#14081,1.);
#3959=VECTOR('',#14084,1.);
#3960=VECTOR('',#14085,1.);
#3961=VECTOR('',#14086,1.);
#3962=VECTOR('',#14089,1.);
#3963=VECTOR('',#14090,1.);
#3964=VECTOR('',#14091,1.);
#3965=VECTOR('',#14094,1.);
#3966=VECTOR('',#14095,1.);
#3967=VECTOR('',#14096,1.);
#3968=VECTOR('',#14099,1.);
#3969=VECTOR('',#14100,1.);
#3970=VECTOR('',#14101,1.);
#3971=VECTOR('',#14104,1.);
#3972=VECTOR('',#14105,1.);
#3973=VECTOR('',#14114,0.35);
#4920=VERTEX_POINT('',#36372);
#4921=VERTEX_POINT('',#36373);
#4922=VERTEX_POINT('',#36375);
#4923=VERTEX_POINT('',#36386);
#4924=VERTEX_POINT('',#36396);
#4925=VERTEX_POINT('',#36397);
#4926=VERTEX_POINT('',#36444);
#4927=VERTEX_POINT('',#36445);
#4928=VERTEX_POINT('',#36492);
#4929=VERTEX_POINT('',#36493);
#4930=VERTEX_POINT('',#36540);
#4931=VERTEX_POINT('',#36541);
#4932=VERTEX_POINT('',#36588);
#4933=VERTEX_POINT('',#36589);
#4934=VERTEX_POINT('',#36636);
#4935=VERTEX_POINT('',#36637);
#4936=VERTEX_POINT('',#36684);
#4937=VERTEX_POINT('',#36685);
#4938=VERTEX_POINT('',#36738);
#4939=VERTEX_POINT('',#36739);
#4940=VERTEX_POINT('',#36786);
#4941=VERTEX_POINT('',#36787);
#4942=VERTEX_POINT('',#36834);
#4943=VERTEX_POINT('',#36835);
#4944=VERTEX_POINT('',#36888);
#4945=VERTEX_POINT('',#36889);
#4946=VERTEX_POINT('',#36936);
#4947=VERTEX_POINT('',#36937);
#4948=VERTEX_POINT('',#36984);
#4949=VERTEX_POINT('',#36985);
#4950=VERTEX_POINT('',#37032);
#4951=VERTEX_POINT('',#37033);
#4952=VERTEX_POINT('',#37083);
#4953=VERTEX_POINT('',#37084);
#4954=VERTEX_POINT('',#37131);
#4955=VERTEX_POINT('',#37132);
#4956=VERTEX_POINT('',#37134);
#4957=VERTEX_POINT('',#37143);
#4958=VERTEX_POINT('',#37153);
#4959=VERTEX_POINT('',#37154);
#4960=VERTEX_POINT('',#37177);
#4961=VERTEX_POINT('',#37178);
#4962=VERTEX_POINT('',#37201);
#4963=VERTEX_POINT('',#37202);
#4964=VERTEX_POINT('',#37227);
#4965=VERTEX_POINT('',#37228);
#4966=VERTEX_POINT('',#37251);
#4967=VERTEX_POINT('',#37252);
#4968=VERTEX_POINT('',#37275);
#4969=VERTEX_POINT('',#37276);
#4970=VERTEX_POINT('',#37300);
#4971=VERTEX_POINT('',#37301);
#4972=VERTEX_POINT('',#37325);
#4973=VERTEX_POINT('',#37326);
#4974=VERTEX_POINT('',#37349);
#4975=VERTEX_POINT('',#37350);
#4976=VERTEX_POINT('',#37374);
#4977=VERTEX_POINT('',#37375);
#4978=VERTEX_POINT('',#37399);
#4979=VERTEX_POINT('',#37400);
#4980=VERTEX_POINT('',#37423);
#4981=VERTEX_POINT('',#37424);
#4982=VERTEX_POINT('',#37447);
#4983=VERTEX_POINT('',#37448);
#4984=VERTEX_POINT('',#37472);
#4985=VERTEX_POINT('',#37473);
#4986=VERTEX_POINT('',#37497);
#4987=VERTEX_POINT('',#37498);
#4988=VERTEX_POINT('',#37521);
#4989=VERTEX_POINT('',#37601);
#4990=VERTEX_POINT('',#37636);
#4991=VERTEX_POINT('',#37702);
#4992=VERTEX_POINT('',#38129);
#4993=VERTEX_POINT('',#38210);
#4994=VERTEX_POINT('',#38723);
#4995=VERTEX_POINT('',#38724);
#4996=VERTEX_POINT('',#38726);
#4997=VERTEX_POINT('',#38728);
#4998=VERTEX_POINT('',#38732);
#4999=VERTEX_POINT('',#38734);
#5000=VERTEX_POINT('',#38738);
#5001=VERTEX_POINT('',#38740);
#5002=VERTEX_POINT('',#38744);
#5003=VERTEX_POINT('',#38746);
#5004=VERTEX_POINT('',#38750);
#5005=VERTEX_POINT('',#38752);
#5006=VERTEX_POINT('',#38760);
#5007=VERTEX_POINT('',#38763);
#6441=EDGE_CURVE('',#4920,#4921,#3290,.T.);
#6442=EDGE_CURVE('',#4920,#4922,#2610,.T.);
#6443=EDGE_CURVE('',#4922,#4923,#1964,.F.);
#6444=EDGE_CURVE('',#4923,#4921,#2611,.T.);
#6445=EDGE_CURVE('',#4924,#4925,#3291,.T.);
#6446=EDGE_CURVE('',#4924,#4920,#2612,.T.);
#6447=EDGE_CURVE('',#4921,#4925,#2613,.T.);
#6448=EDGE_CURVE('',#4926,#4927,#3292,.T.);
#6449=EDGE_CURVE('',#4926,#4924,#2614,.T.);
#6450=EDGE_CURVE('',#4925,#4927,#2615,.T.);
#6451=EDGE_CURVE('',#4928,#4929,#3293,.T.);
#6452=EDGE_CURVE('',#4928,#4926,#2616,.T.);
#6453=EDGE_CURVE('',#4927,#4929,#2617,.T.);
#6454=EDGE_CURVE('',#4930,#4931,#3294,.T.);
#6455=EDGE_CURVE('',#4930,#4928,#2618,.T.);
#6456=EDGE_CURVE('',#4929,#4931,#2619,.T.);
#6457=EDGE_CURVE('',#4932,#4933,#3295,.T.);
#6458=EDGE_CURVE('',#4932,#4930,#2620,.T.);
#6459=EDGE_CURVE('',#4931,#4933,#2621,.T.);
#6460=EDGE_CURVE('',#4934,#4935,#3296,.T.);
#6461=EDGE_CURVE('',#4934,#4932,#2622,.T.);
#6462=EDGE_CURVE('',#4933,#4935,#2623,.T.);
#6463=EDGE_CURVE('',#4936,#4937,#3297,.T.);
#6464=EDGE_CURVE('',#4936,#4934,#2624,.T.);
#6465=EDGE_CURVE('',#4935,#4937,#2625,.T.);
#6466=EDGE_CURVE('',#4938,#4939,#3298,.T.);
#6467=EDGE_CURVE('',#4938,#4936,#2626,.T.);
#6468=EDGE_CURVE('',#4937,#4939,#2627,.T.);
#6469=EDGE_CURVE('',#4940,#4941,#3299,.T.);
#6470=EDGE_CURVE('',#4940,#4938,#2628,.T.);
#6471=EDGE_CURVE('',#4939,#4941,#2629,.T.);
#6472=EDGE_CURVE('',#4942,#4943,#3300,.T.);
#6473=EDGE_CURVE('',#4942,#4940,#2630,.T.);
#6474=EDGE_CURVE('',#4941,#4943,#2631,.T.);
#6475=EDGE_CURVE('',#4944,#4945,#3301,.T.);
#6476=EDGE_CURVE('',#4944,#4942,#2632,.T.);
#6477=EDGE_CURVE('',#4943,#4945,#2633,.T.);
#6478=EDGE_CURVE('',#4946,#4947,#3302,.T.);
#6479=EDGE_CURVE('',#4946,#4944,#2634,.T.);
#6480=EDGE_CURVE('',#4945,#4947,#2635,.T.);
#6481=EDGE_CURVE('',#4948,#4949,#3303,.T.);
#6482=EDGE_CURVE('',#4948,#4946,#2636,.T.);
#6483=EDGE_CURVE('',#4947,#4949,#2637,.T.);
#6484=EDGE_CURVE('',#4950,#4951,#3304,.T.);
#6485=EDGE_CURVE('',#4950,#4948,#2638,.T.);
#6486=EDGE_CURVE('',#4949,#4951,#2639,.T.);
#6487=EDGE_CURVE('',#4952,#4953,#3305,.T.);
#6488=EDGE_CURVE('',#4952,#4950,#2640,.T.);
#6489=EDGE_CURVE('',#4951,#4953,#2641,.T.);
#6490=EDGE_CURVE('',#4954,#4955,#3306,.T.);
#6491=EDGE_CURVE('',#4954,#4956,#2642,.T.);
#6492=EDGE_CURVE('',#4956,#4957,#1965,.T.);
#6493=EDGE_CURVE('',#4955,#4957,#2643,.T.);
#6494=EDGE_CURVE('',#4958,#4959,#3307,.T.);
#6495=EDGE_CURVE('',#4958,#4954,#2644,.T.);
#6496=EDGE_CURVE('',#4959,#4955,#2645,.T.);
#6497=EDGE_CURVE('',#4960,#4961,#3308,.T.);
#6498=EDGE_CURVE('',#4960,#4958,#2646,.T.);
#6499=EDGE_CURVE('',#4961,#4959,#2647,.T.);
#6500=EDGE_CURVE('',#4962,#4963,#3309,.T.);
#6501=EDGE_CURVE('',#4962,#4960,#2648,.T.);
#6502=EDGE_CURVE('',#4963,#4961,#2649,.T.);
#6503=EDGE_CURVE('',#4964,#4965,#3310,.T.);
#6504=EDGE_CURVE('',#4964,#4962,#2650,.T.);
#6505=EDGE_CURVE('',#4965,#4963,#2651,.T.);
#6506=EDGE_CURVE('',#4966,#4967,#3311,.T.);
#6507=EDGE_CURVE('',#4966,#4964,#2652,.T.);
#6508=EDGE_CURVE('',#4967,#4965,#2653,.T.);
#6509=EDGE_CURVE('',#4968,#4969,#3312,.T.);
#6510=EDGE_CURVE('',#4968,#4966,#2654,.T.);
#6511=EDGE_CURVE('',#4969,#4967,#2655,.T.);
#6512=EDGE_CURVE('',#4970,#4971,#3313,.T.);
#6513=EDGE_CURVE('',#4970,#4968,#2656,.T.);
#6514=EDGE_CURVE('',#4971,#4969,#2657,.T.);
#6515=EDGE_CURVE('',#4972,#4973,#3314,.T.);
#6516=EDGE_CURVE('',#4972,#4970,#2658,.T.);
#6517=EDGE_CURVE('',#4973,#4971,#2659,.T.);
#6518=EDGE_CURVE('',#4974,#4975,#3315,.T.);
#6519=EDGE_CURVE('',#4974,#4972,#2660,.T.);
#6520=EDGE_CURVE('',#4975,#4973,#2661,.T.);
#6521=EDGE_CURVE('',#4976,#4977,#3316,.T.);
#6522=EDGE_CURVE('',#4976,#4974,#2662,.T.);
#6523=EDGE_CURVE('',#4977,#4975,#2663,.T.);
#6524=EDGE_CURVE('',#4978,#4979,#3317,.T.);
#6525=EDGE_CURVE('',#4978,#4976,#2664,.T.);
#6526=EDGE_CURVE('',#4979,#4977,#2665,.T.);
#6527=EDGE_CURVE('',#4980,#4981,#3318,.T.);
#6528=EDGE_CURVE('',#4980,#4978,#2666,.T.);
#6529=EDGE_CURVE('',#4981,#4979,#2667,.T.);
#6530=EDGE_CURVE('',#4982,#4983,#3319,.T.);
#6531=EDGE_CURVE('',#4982,#4980,#2668,.T.);
#6532=EDGE_CURVE('',#4983,#4981,#2669,.T.);
#6533=EDGE_CURVE('',#4984,#4985,#3320,.T.);
#6534=EDGE_CURVE('',#4984,#4982,#2670,.T.);
#6535=EDGE_CURVE('',#4985,#4983,#2671,.T.);
#6536=EDGE_CURVE('',#4986,#4987,#3321,.T.);
#6537=EDGE_CURVE('',#4986,#4984,#2672,.T.);
#6538=EDGE_CURVE('',#4987,#4985,#2673,.T.);
#6539=EDGE_CURVE('',#4957,#4988,#2674,.T.);
#6540=EDGE_CURVE('',#4989,#4956,#2675,.T.);
#6541=EDGE_CURVE('',#4990,#4989,#1966,.T.);
#6542=EDGE_CURVE('',#4988,#4990,#2676,.T.);
#6543=EDGE_CURVE('',#4988,#4991,#3322,.T.);
#6544=EDGE_CURVE('',#4991,#4991,#1967,.T.);
#6545=EDGE_CURVE('',#4992,#4986,#2677,.T.);
#6546=EDGE_CURVE('',#4922,#4992,#2678,.T.);
#6547=EDGE_CURVE('',#4989,#4952,#2679,.T.);
#6548=EDGE_CURVE('',#4993,#4987,#2680,.T.);
#6549=EDGE_CURVE('',#4992,#4993,#1968,.T.);
#6550=EDGE_CURVE('',#4953,#4990,#2681,.T.);
#6551=EDGE_CURVE('',#4993,#4923,#2682,.T.);
#6552=EDGE_CURVE('',#4994,#4995,#3323,.T.);
#6553=EDGE_CURVE('',#4994,#4996,#3324,.T.);
#6554=EDGE_CURVE('',#4996,#4997,#3325,.T.);
#6555=EDGE_CURVE('',#4995,#4997,#3326,.T.);
#6556=EDGE_CURVE('',#4998,#4994,#3327,.T.);
#6557=EDGE_CURVE('',#4998,#4999,#3328,.T.);
#6558=EDGE_CURVE('',#4999,#4996,#3329,.T.);
#6559=EDGE_CURVE('',#5000,#4998,#3330,.T.);
#6560=EDGE_CURVE('',#5000,#5001,#3331,.T.);
#6561=EDGE_CURVE('',#5001,#4999,#3332,.T.);
#6562=EDGE_CURVE('',#5002,#5000,#3333,.T.);
#6563=EDGE_CURVE('',#5002,#5003,#3334,.T.);
#6564=EDGE_CURVE('',#5003,#5001,#3335,.T.);
#6565=EDGE_CURVE('',#5004,#5002,#3336,.T.);
#6566=EDGE_CURVE('',#5004,#5005,#3337,.T.);
#6567=EDGE_CURVE('',#5005,#5003,#3338,.T.);
#6568=EDGE_CURVE('',#4995,#5004,#3339,.T.);
#6569=EDGE_CURVE('',#4997,#5005,#3340,.T.);
#6570=EDGE_CURVE('',#5006,#5006,#1969,.T.);
#6571=EDGE_CURVE('',#5006,#5007,#3341,.T.);
#6572=EDGE_CURVE('',#5007,#5007,#1970,.T.);
#9343=ORIENTED_EDGE('',*,*,#6441,.F.);
#9344=ORIENTED_EDGE('',*,*,#6442,.T.);
#9345=ORIENTED_EDGE('',*,*,#6443,.T.);
#9346=ORIENTED_EDGE('',*,*,#6444,.T.);
#9347=ORIENTED_EDGE('',*,*,#6445,.F.);
#9348=ORIENTED_EDGE('',*,*,#6446,.T.);
#9349=ORIENTED_EDGE('',*,*,#6441,.T.);
#9350=ORIENTED_EDGE('',*,*,#6447,.T.);
#9351=ORIENTED_EDGE('',*,*,#6448,.F.);
#9352=ORIENTED_EDGE('',*,*,#6449,.T.);
#9353=ORIENTED_EDGE('',*,*,#6445,.T.);
#9354=ORIENTED_EDGE('',*,*,#6450,.T.);
#9355=ORIENTED_EDGE('',*,*,#6451,.F.);
#9356=ORIENTED_EDGE('',*,*,#6452,.T.);
#9357=ORIENTED_EDGE('',*,*,#6448,.T.);
#9358=ORIENTED_EDGE('',*,*,#6453,.T.);
#9359=ORIENTED_EDGE('',*,*,#6454,.F.);
#9360=ORIENTED_EDGE('',*,*,#6455,.T.);
#9361=ORIENTED_EDGE('',*,*,#6451,.T.);
#9362=ORIENTED_EDGE('',*,*,#6456,.T.);
#9363=ORIENTED_EDGE('',*,*,#6457,.F.);
#9364=ORIENTED_EDGE('',*,*,#6458,.T.);
#9365=ORIENTED_EDGE('',*,*,#6454,.T.);
#9366=ORIENTED_EDGE('',*,*,#6459,.T.);
#9367=ORIENTED_EDGE('',*,*,#6460,.F.);
#9368=ORIENTED_EDGE('',*,*,#6461,.T.);
#9369=ORIENTED_EDGE('',*,*,#6457,.T.);
#9370=ORIENTED_EDGE('',*,*,#6462,.T.);
#9371=ORIENTED_EDGE('',*,*,#6463,.F.);
#9372=ORIENTED_EDGE('',*,*,#6464,.T.);
#9373=ORIENTED_EDGE('',*,*,#6460,.T.);
#9374=ORIENTED_EDGE('',*,*,#6465,.T.);
#9375=ORIENTED_EDGE('',*,*,#6466,.F.);
#9376=ORIENTED_EDGE('',*,*,#6467,.T.);
#9377=ORIENTED_EDGE('',*,*,#6463,.T.);
#9378=ORIENTED_EDGE('',*,*,#6468,.T.);
#9379=ORIENTED_EDGE('',*,*,#6469,.F.);
#9380=ORIENTED_EDGE('',*,*,#6470,.T.);
#9381=ORIENTED_EDGE('',*,*,#6466,.T.);
#9382=ORIENTED_EDGE('',*,*,#6471,.T.);
#9383=ORIENTED_EDGE('',*,*,#6472,.F.);
#9384=ORIENTED_EDGE('',*,*,#6473,.T.);
#9385=ORIENTED_EDGE('',*,*,#6469,.T.);
#9386=ORIENTED_EDGE('',*,*,#6474,.T.);
#9387=ORIENTED_EDGE('',*,*,#6475,.F.);
#9388=ORIENTED_EDGE('',*,*,#6476,.T.);
#9389=ORIENTED_EDGE('',*,*,#6472,.T.);
#9390=ORIENTED_EDGE('',*,*,#6477,.T.);
#9391=ORIENTED_EDGE('',*,*,#6478,.F.);
#9392=ORIENTED_EDGE('',*,*,#6479,.T.);
#9393=ORIENTED_EDGE('',*,*,#6475,.T.);
#9394=ORIENTED_EDGE('',*,*,#6480,.T.);
#9395=ORIENTED_EDGE('',*,*,#6481,.F.);
#9396=ORIENTED_EDGE('',*,*,#6482,.T.);
#9397=ORIENTED_EDGE('',*,*,#6478,.T.);
#9398=ORIENTED_EDGE('',*,*,#6483,.T.);
#9399=ORIENTED_EDGE('',*,*,#6484,.F.);
#9400=ORIENTED_EDGE('',*,*,#6485,.T.);
#9401=ORIENTED_EDGE('',*,*,#6481,.T.);
#9402=ORIENTED_EDGE('',*,*,#6486,.T.);
#9403=ORIENTED_EDGE('',*,*,#6487,.F.);
#9404=ORIENTED_EDGE('',*,*,#6488,.T.);
#9405=ORIENTED_EDGE('',*,*,#6484,.T.);
#9406=ORIENTED_EDGE('',*,*,#6489,.T.);
#9407=ORIENTED_EDGE('',*,*,#6490,.F.);
#9408=ORIENTED_EDGE('',*,*,#6491,.T.);
#9409=ORIENTED_EDGE('',*,*,#6492,.T.);
#9410=ORIENTED_EDGE('',*,*,#6493,.F.);
#9411=ORIENTED_EDGE('',*,*,#6494,.F.);
#9412=ORIENTED_EDGE('',*,*,#6495,.T.);
#9413=ORIENTED_EDGE('',*,*,#6490,.T.);
#9414=ORIENTED_EDGE('',*,*,#6496,.F.);
#9415=ORIENTED_EDGE('',*,*,#6497,.F.);
#9416=ORIENTED_EDGE('',*,*,#6498,.T.);
#9417=ORIENTED_EDGE('',*,*,#6494,.T.);
#9418=ORIENTED_EDGE('',*,*,#6499,.F.);
#9419=ORIENTED_EDGE('',*,*,#6500,.F.);
#9420=ORIENTED_EDGE('',*,*,#6501,.T.);
#9421=ORIENTED_EDGE('',*,*,#6497,.T.);
#9422=ORIENTED_EDGE('',*,*,#6502,.F.);
#9423=ORIENTED_EDGE('',*,*,#6503,.F.);
#9424=ORIENTED_EDGE('',*,*,#6504,.T.);
#9425=ORIENTED_EDGE('',*,*,#6500,.T.);
#9426=ORIENTED_EDGE('',*,*,#6505,.F.);
#9427=ORIENTED_EDGE('',*,*,#6506,.F.);
#9428=ORIENTED_EDGE('',*,*,#6507,.T.);
#9429=ORIENTED_EDGE('',*,*,#6503,.T.);
#9430=ORIENTED_EDGE('',*,*,#6508,.F.);
#9431=ORIENTED_EDGE('',*,*,#6509,.F.);
#9432=ORIENTED_EDGE('',*,*,#6510,.T.);
#9433=ORIENTED_EDGE('',*,*,#6506,.T.);
#9434=ORIENTED_EDGE('',*,*,#6511,.F.);
#9435=ORIENTED_EDGE('',*,*,#6512,.F.);
#9436=ORIENTED_EDGE('',*,*,#6513,.T.);
#9437=ORIENTED_EDGE('',*,*,#6509,.T.);
#9438=ORIENTED_EDGE('',*,*,#6514,.F.);
#9439=ORIENTED_EDGE('',*,*,#6515,.F.);
#9440=ORIENTED_EDGE('',*,*,#6516,.T.);
#9441=ORIENTED_EDGE('',*,*,#6512,.T.);
#9442=ORIENTED_EDGE('',*,*,#6517,.F.);
#9443=ORIENTED_EDGE('',*,*,#6518,.F.);
#9444=ORIENTED_EDGE('',*,*,#6519,.T.);
#9445=ORIENTED_EDGE('',*,*,#6515,.T.);
#9446=ORIENTED_EDGE('',*,*,#6520,.F.);
#9447=ORIENTED_EDGE('',*,*,#6521,.F.);
#9448=ORIENTED_EDGE('',*,*,#6522,.T.);
#9449=ORIENTED_EDGE('',*,*,#6518,.T.);
#9450=ORIENTED_EDGE('',*,*,#6523,.F.);
#9451=ORIENTED_EDGE('',*,*,#6524,.F.);
#9452=ORIENTED_EDGE('',*,*,#6525,.T.);
#9453=ORIENTED_EDGE('',*,*,#6521,.T.);
#9454=ORIENTED_EDGE('',*,*,#6526,.F.);
#9455=ORIENTED_EDGE('',*,*,#6527,.F.);
#9456=ORIENTED_EDGE('',*,*,#6528,.T.);
#9457=ORIENTED_EDGE('',*,*,#6524,.T.);
#9458=ORIENTED_EDGE('',*,*,#6529,.F.);
#9459=ORIENTED_EDGE('',*,*,#6530,.F.);
#9460=ORIENTED_EDGE('',*,*,#6531,.T.);
#9461=ORIENTED_EDGE('',*,*,#6527,.T.);
#9462=ORIENTED_EDGE('',*,*,#6532,.F.);
#9463=ORIENTED_EDGE('',*,*,#6533,.F.);
#9464=ORIENTED_EDGE('',*,*,#6534,.T.);
#9465=ORIENTED_EDGE('',*,*,#6530,.T.);
#9466=ORIENTED_EDGE('',*,*,#6535,.F.);
#9467=ORIENTED_EDGE('',*,*,#6536,.F.);
#9468=ORIENTED_EDGE('',*,*,#6537,.T.);
#9469=ORIENTED_EDGE('',*,*,#6533,.T.);
#9470=ORIENTED_EDGE('',*,*,#6538,.F.);
#9471=ORIENTED_EDGE('',*,*,#6539,.F.);
#9472=ORIENTED_EDGE('',*,*,#6492,.F.);
#9473=ORIENTED_EDGE('',*,*,#6540,.F.);
#9474=ORIENTED_EDGE('',*,*,#6541,.F.);
#9475=ORIENTED_EDGE('',*,*,#6542,.F.);
#9476=ORIENTED_EDGE('',*,*,#6543,.T.);
#9477=ORIENTED_EDGE('',*,*,#6544,.F.);
#9478=ORIENTED_EDGE('',*,*,#6543,.F.);
#9479=ORIENTED_EDGE('',*,*,#6540,.T.);
#9480=ORIENTED_EDGE('',*,*,#6491,.F.);
#9481=ORIENTED_EDGE('',*,*,#6495,.F.);
#9482=ORIENTED_EDGE('',*,*,#6498,.F.);
#9483=ORIENTED_EDGE('',*,*,#6501,.F.);
#9484=ORIENTED_EDGE('',*,*,#6504,.F.);
#9485=ORIENTED_EDGE('',*,*,#6507,.F.);
#9486=ORIENTED_EDGE('',*,*,#6510,.F.);
#9487=ORIENTED_EDGE('',*,*,#6513,.F.);
#9488=ORIENTED_EDGE('',*,*,#6516,.F.);
#9489=ORIENTED_EDGE('',*,*,#6519,.F.);
#9490=ORIENTED_EDGE('',*,*,#6522,.F.);
#9491=ORIENTED_EDGE('',*,*,#6525,.F.);
#9492=ORIENTED_EDGE('',*,*,#6528,.F.);
#9493=ORIENTED_EDGE('',*,*,#6531,.F.);
#9494=ORIENTED_EDGE('',*,*,#6534,.F.);
#9495=ORIENTED_EDGE('',*,*,#6537,.F.);
#9496=ORIENTED_EDGE('',*,*,#6545,.F.);
#9497=ORIENTED_EDGE('',*,*,#6546,.F.);
#9498=ORIENTED_EDGE('',*,*,#6442,.F.);
#9499=ORIENTED_EDGE('',*,*,#6446,.F.);
#9500=ORIENTED_EDGE('',*,*,#6449,.F.);
#9501=ORIENTED_EDGE('',*,*,#6452,.F.);
#9502=ORIENTED_EDGE('',*,*,#6455,.F.);
#9503=ORIENTED_EDGE('',*,*,#6458,.F.);
#9504=ORIENTED_EDGE('',*,*,#6461,.F.);
#9505=ORIENTED_EDGE('',*,*,#6464,.F.);
#9506=ORIENTED_EDGE('',*,*,#6467,.F.);
#9507=ORIENTED_EDGE('',*,*,#6470,.F.);
#9508=ORIENTED_EDGE('',*,*,#6473,.F.);
#9509=ORIENTED_EDGE('',*,*,#6476,.F.);
#9510=ORIENTED_EDGE('',*,*,#6479,.F.);
#9511=ORIENTED_EDGE('',*,*,#6482,.F.);
#9512=ORIENTED_EDGE('',*,*,#6485,.F.);
#9513=ORIENTED_EDGE('',*,*,#6488,.F.);
#9514=ORIENTED_EDGE('',*,*,#6547,.F.);
#9515=ORIENTED_EDGE('',*,*,#6536,.T.);
#9516=ORIENTED_EDGE('',*,*,#6548,.F.);
#9517=ORIENTED_EDGE('',*,*,#6549,.F.);
#9518=ORIENTED_EDGE('',*,*,#6545,.T.);
#9519=ORIENTED_EDGE('',*,*,#6539,.T.);
#9520=ORIENTED_EDGE('',*,*,#6542,.T.);
#9521=ORIENTED_EDGE('',*,*,#6550,.F.);
#9522=ORIENTED_EDGE('',*,*,#6489,.F.);
#9523=ORIENTED_EDGE('',*,*,#6486,.F.);
#9524=ORIENTED_EDGE('',*,*,#6483,.F.);
#9525=ORIENTED_EDGE('',*,*,#6480,.F.);
#9526=ORIENTED_EDGE('',*,*,#6477,.F.);
#9527=ORIENTED_EDGE('',*,*,#6474,.F.);
#9528=ORIENTED_EDGE('',*,*,#6471,.F.);
#9529=ORIENTED_EDGE('',*,*,#6468,.F.);
#9530=ORIENTED_EDGE('',*,*,#6465,.F.);
#9531=ORIENTED_EDGE('',*,*,#6462,.F.);
#9532=ORIENTED_EDGE('',*,*,#6459,.F.);
#9533=ORIENTED_EDGE('',*,*,#6456,.F.);
#9534=ORIENTED_EDGE('',*,*,#6453,.F.);
#9535=ORIENTED_EDGE('',*,*,#6450,.F.);
#9536=ORIENTED_EDGE('',*,*,#6447,.F.);
#9537=ORIENTED_EDGE('',*,*,#6444,.F.);
#9538=ORIENTED_EDGE('',*,*,#6551,.F.);
#9539=ORIENTED_EDGE('',*,*,#6548,.T.);
#9540=ORIENTED_EDGE('',*,*,#6538,.T.);
#9541=ORIENTED_EDGE('',*,*,#6535,.T.);
#9542=ORIENTED_EDGE('',*,*,#6532,.T.);
#9543=ORIENTED_EDGE('',*,*,#6529,.T.);
#9544=ORIENTED_EDGE('',*,*,#6526,.T.);
#9545=ORIENTED_EDGE('',*,*,#6523,.T.);
#9546=ORIENTED_EDGE('',*,*,#6520,.T.);
#9547=ORIENTED_EDGE('',*,*,#6517,.T.);
#9548=ORIENTED_EDGE('',*,*,#6514,.T.);
#9549=ORIENTED_EDGE('',*,*,#6511,.T.);
#9550=ORIENTED_EDGE('',*,*,#6508,.T.);
#9551=ORIENTED_EDGE('',*,*,#6505,.T.);
#9552=ORIENTED_EDGE('',*,*,#6502,.T.);
#9553=ORIENTED_EDGE('',*,*,#6499,.T.);
#9554=ORIENTED_EDGE('',*,*,#6496,.T.);
#9555=ORIENTED_EDGE('',*,*,#6493,.T.);
#9556=ORIENTED_EDGE('',*,*,#6487,.T.);
#9557=ORIENTED_EDGE('',*,*,#6550,.T.);
#9558=ORIENTED_EDGE('',*,*,#6541,.T.);
#9559=ORIENTED_EDGE('',*,*,#6547,.T.);
#9560=ORIENTED_EDGE('',*,*,#6552,.F.);
#9561=ORIENTED_EDGE('',*,*,#6553,.T.);
#9562=ORIENTED_EDGE('',*,*,#6554,.T.);
#9563=ORIENTED_EDGE('',*,*,#6555,.F.);
#9564=ORIENTED_EDGE('',*,*,#6556,.F.);
#9565=ORIENTED_EDGE('',*,*,#6557,.T.);
#9566=ORIENTED_EDGE('',*,*,#6558,.T.);
#9567=ORIENTED_EDGE('',*,*,#6553,.F.);
#9568=ORIENTED_EDGE('',*,*,#6559,.F.);
#9569=ORIENTED_EDGE('',*,*,#6560,.T.);
#9570=ORIENTED_EDGE('',*,*,#6561,.T.);
#9571=ORIENTED_EDGE('',*,*,#6557,.F.);
#9572=ORIENTED_EDGE('',*,*,#6562,.F.);
#9573=ORIENTED_EDGE('',*,*,#6563,.T.);
#9574=ORIENTED_EDGE('',*,*,#6564,.T.);
#9575=ORIENTED_EDGE('',*,*,#6560,.F.);
#9576=ORIENTED_EDGE('',*,*,#6565,.F.);
#9577=ORIENTED_EDGE('',*,*,#6566,.T.);
#9578=ORIENTED_EDGE('',*,*,#6567,.T.);
#9579=ORIENTED_EDGE('',*,*,#6563,.F.);
#9580=ORIENTED_EDGE('',*,*,#6568,.F.);
#9581=ORIENTED_EDGE('',*,*,#6555,.T.);
#9582=ORIENTED_EDGE('',*,*,#6569,.T.);
#9583=ORIENTED_EDGE('',*,*,#6566,.F.);
#9584=ORIENTED_EDGE('',*,*,#6569,.F.);
#9585=ORIENTED_EDGE('',*,*,#6554,.F.);
#9586=ORIENTED_EDGE('',*,*,#6558,.F.);
#9587=ORIENTED_EDGE('',*,*,#6561,.F.);
#9588=ORIENTED_EDGE('',*,*,#6564,.F.);
#9589=ORIENTED_EDGE('',*,*,#6567,.F.);
#9590=ORIENTED_EDGE('',*,*,#6570,.T.);
#9591=ORIENTED_EDGE('',*,*,#6546,.T.);
#9592=ORIENTED_EDGE('',*,*,#6549,.T.);
#9593=ORIENTED_EDGE('',*,*,#6551,.T.);
#9594=ORIENTED_EDGE('',*,*,#6443,.F.);
#9595=ORIENTED_EDGE('',*,*,#6570,.F.);
#9596=ORIENTED_EDGE('',*,*,#6571,.T.);
#9597=ORIENTED_EDGE('',*,*,#6572,.T.);
#9598=ORIENTED_EDGE('',*,*,#6571,.F.);
#9599=ORIENTED_EDGE('',*,*,#6572,.F.);
#9600=ORIENTED_EDGE('',*,*,#6552,.T.);
#9601=ORIENTED_EDGE('',*,*,#6568,.T.);
#9602=ORIENTED_EDGE('',*,*,#6565,.T.);
#9603=ORIENTED_EDGE('',*,*,#6562,.T.);
#9604=ORIENTED_EDGE('',*,*,#6559,.T.);
#9605=ORIENTED_EDGE('',*,*,#6556,.T.);
#9606=ORIENTED_EDGE('',*,*,#6544,.T.);
#10505=CYLINDRICAL_SURFACE('',#12054,0.1954);
#10506=CYLINDRICAL_SURFACE('',#12056,0.1954);
#10507=CYLINDRICAL_SURFACE('',#12057,0.1954);
#10508=CYLINDRICAL_SURFACE('',#12058,0.1954);
#10509=CYLINDRICAL_SURFACE('',#12059,0.1954);
#10510=CYLINDRICAL_SURFACE('',#12060,0.1954);
#10511=CYLINDRICAL_SURFACE('',#12061,0.1954);
#10512=CYLINDRICAL_SURFACE('',#12062,0.1954);
#10513=CYLINDRICAL_SURFACE('',#12063,0.1954);
#10514=CYLINDRICAL_SURFACE('',#12064,0.1954);
#10515=CYLINDRICAL_SURFACE('',#12065,0.1954);
#10516=CYLINDRICAL_SURFACE('',#12066,0.1954);
#10517=CYLINDRICAL_SURFACE('',#12067,0.1954);
#10518=CYLINDRICAL_SURFACE('',#12068,0.1954);
#10519=CYLINDRICAL_SURFACE('',#12069,0.1954);
#10520=CYLINDRICAL_SURFACE('',#12070,0.1954);
#10521=CYLINDRICAL_SURFACE('',#12071,0.15555);
#10522=CYLINDRICAL_SURFACE('',#12073,0.15555);
#10523=CYLINDRICAL_SURFACE('',#12074,0.15555);
#10524=CYLINDRICAL_SURFACE('',#12075,0.15555);
#10525=CYLINDRICAL_SURFACE('',#12076,0.15555);
#10526=CYLINDRICAL_SURFACE('',#12077,0.15555);
#10527=CYLINDRICAL_SURFACE('',#12078,0.15555);
#10528=CYLINDRICAL_SURFACE('',#12079,0.15555);
#10529=CYLINDRICAL_SURFACE('',#12080,0.15555);
#10530=CYLINDRICAL_SURFACE('',#12081,0.15555);
#10531=CYLINDRICAL_SURFACE('',#12082,0.15555);
#10532=CYLINDRICAL_SURFACE('',#12083,0.15555);
#10533=CYLINDRICAL_SURFACE('',#12084,0.15555);
#10534=CYLINDRICAL_SURFACE('',#12085,0.15555);
#10535=CYLINDRICAL_SURFACE('',#12086,0.15555);
#10536=CYLINDRICAL_SURFACE('',#12087,0.15555);
#10537=CYLINDRICAL_SURFACE('',#12091,0.15555);
#10538=CYLINDRICAL_SURFACE('',#12093,0.1954);
#10539=CYLINDRICAL_SURFACE('',#12103,0.35);
#11075=ADVANCED_FACE('',(#950),#10505,.T.);
#11076=ADVANCED_FACE('',(#951),#10506,.T.);
#11077=ADVANCED_FACE('',(#952),#10507,.T.);
#11078=ADVANCED_FACE('',(#953),#10508,.T.);
#11079=ADVANCED_FACE('',(#954),#10509,.T.);
#11080=ADVANCED_FACE('',(#955),#10510,.T.);
#11081=ADVANCED_FACE('',(#956),#10511,.T.);
#11082=ADVANCED_FACE('',(#957),#10512,.T.);
#11083=ADVANCED_FACE('',(#958),#10513,.T.);
#11084=ADVANCED_FACE('',(#959),#10514,.T.);
#11085=ADVANCED_FACE('',(#960),#10515,.T.);
#11086=ADVANCED_FACE('',(#961),#10516,.T.);
#11087=ADVANCED_FACE('',(#962),#10517,.T.);
#11088=ADVANCED_FACE('',(#963),#10518,.T.);
#11089=ADVANCED_FACE('',(#964),#10519,.T.);
#11090=ADVANCED_FACE('',(#965),#10520,.T.);
#11091=ADVANCED_FACE('',(#966),#10521,.T.);
#11092=ADVANCED_FACE('',(#967),#10522,.T.);
#11093=ADVANCED_FACE('',(#968),#10523,.T.);
#11094=ADVANCED_FACE('',(#969),#10524,.T.);
#11095=ADVANCED_FACE('',(#970),#10525,.T.);
#11096=ADVANCED_FACE('',(#971),#10526,.T.);
#11097=ADVANCED_FACE('',(#972),#10527,.T.);
#11098=ADVANCED_FACE('',(#973),#10528,.T.);
#11099=ADVANCED_FACE('',(#974),#10529,.T.);
#11100=ADVANCED_FACE('',(#975),#10530,.T.);
#11101=ADVANCED_FACE('',(#976),#10531,.T.);
#11102=ADVANCED_FACE('',(#977),#10532,.T.);
#11103=ADVANCED_FACE('',(#978),#10533,.T.);
#11104=ADVANCED_FACE('',(#979),#10534,.T.);
#11105=ADVANCED_FACE('',(#980),#10535,.T.);
#11106=ADVANCED_FACE('',(#981),#10536,.T.);
#11107=ADVANCED_FACE('',(#982),#147,.T.);
#11108=ADVANCED_FACE('',(#983),#250,.F.);
#11109=ADVANCED_FACE('',(#984),#10537,.T.);
#11110=ADVANCED_FACE('',(#985),#251,.F.);
#11111=ADVANCED_FACE('',(#986),#10538,.T.);
#11112=ADVANCED_FACE('',(#987),#444,.F.);
#11113=ADVANCED_FACE('',(#988),#445,.F.);
#11114=ADVANCED_FACE('',(#989),#446,.F.);
#11115=ADVANCED_FACE('',(#990),#447,.F.);
#11116=ADVANCED_FACE('',(#991),#448,.F.);
#11117=ADVANCED_FACE('',(#992),#449,.F.);
#11118=ADVANCED_FACE('',(#993),#450,.F.);
#11119=ADVANCED_FACE('',(#994,#323),#451,.T.);
#11120=ADVANCED_FACE('',(#995),#10539,.T.);
#11121=ADVANCED_FACE('',(#996,#324),#452,.F.);
#11122=ADVANCED_FACE('',(#997),#453,.T.);
#11244=CLOSED_SHELL('',(#11075,#11076,#11077,#11078,#11079,#11080,#11081,
#11082,#11083,#11084,#11085,#11086,#11087,#11088,#11089,#11090,#11091,#11092,
#11093,#11094,#11095,#11096,#11097,#11098,#11099,#11100,#11101,#11102,#11103,
#11104,#11105,#11106,#11107,#11108,#11109,#11110,#11111,#11112,#11113,#11114,
#11115,#11116,#11117,#11118,#11119,#11120,#11121,#11122));
#12053=AXIS2_PLACEMENT_3D('',#36370,#13961,#13962);
#12054=AXIS2_PLACEMENT_3D('',#36371,#13963,#13964);
#12055=AXIS2_PLACEMENT_3D('',#36387,#13966,#13967);
#12056=AXIS2_PLACEMENT_3D('',#36395,#13968,#13969);
#12057=AXIS2_PLACEMENT_3D('',#36443,#13971,#13972);
#12058=AXIS2_PLACEMENT_3D('',#36491,#13974,#13975);
#12059=AXIS2_PLACEMENT_3D('',#36539,#13977,#13978);
#12060=AXIS2_PLACEMENT_3D('',#36587,#13980,#13981);
#12061=AXIS2_PLACEMENT_3D('',#36635,#13983,#13984);
#12062=AXIS2_PLACEMENT_3D('',#36683,#13986,#13987);
#12063=AXIS2_PLACEMENT_3D('',#36737,#13989,#13990);
#12064=AXIS2_PLACEMENT_3D('',#36785,#13992,#13993);
#12065=AXIS2_PLACEMENT_3D('',#36833,#13995,#13996);
#12066=AXIS2_PLACEMENT_3D('',#36887,#13998,#13999);
#12067=AXIS2_PLACEMENT_3D('',#36935,#14001,#14002);
#12068=AXIS2_PLACEMENT_3D('',#36983,#14004,#14005);
#12069=AXIS2_PLACEMENT_3D('',#37031,#14007,#14008);
#12070=AXIS2_PLACEMENT_3D('',#37082,#14010,#14011);
#12071=AXIS2_PLACEMENT_3D('',#37130,#14013,#14014);
#12072=AXIS2_PLACEMENT_3D('',#37144,#14016,#14017);
#12073=AXIS2_PLACEMENT_3D('',#37152,#14018,#14019);
#12074=AXIS2_PLACEMENT_3D('',#37176,#14021,#14022);
#12075=AXIS2_PLACEMENT_3D('',#37200,#14024,#14025);
#12076=AXIS2_PLACEMENT_3D('',#37226,#14027,#14028);
#12077=AXIS2_PLACEMENT_3D('',#37250,#14030,#14031);
#12078=AXIS2_PLACEMENT_3D('',#37274,#14033,#14034);
#12079=AXIS2_PLACEMENT_3D('',#37299,#14036,#14037);
#12080=AXIS2_PLACEMENT_3D('',#37324,#14039,#14040);
#12081=AXIS2_PLACEMENT_3D('',#37348,#14042,#14043);
#12082=AXIS2_PLACEMENT_3D('',#37373,#14045,#14046);
#12083=AXIS2_PLACEMENT_3D('',#37398,#14048,#14049);
#12084=AXIS2_PLACEMENT_3D('',#37422,#14051,#14052);
#12085=AXIS2_PLACEMENT_3D('',#37446,#14054,#14055);
#12086=AXIS2_PLACEMENT_3D('',#37471,#14057,#14058);
#12087=AXIS2_PLACEMENT_3D('',#37496,#14060,#14061);
#12088=AXIS2_PLACEMENT_3D('',#37520,#14063,#14064);
#12089=AXIS2_PLACEMENT_3D('',#37637,#14065,#14066);
#12090=AXIS2_PLACEMENT_3D('',#37704,#14068,#14069);
#12091=AXIS2_PLACEMENT_3D('',#38209,#14070,#14071);
#12092=AXIS2_PLACEMENT_3D('',#38220,#14072,#14073);
#12093=AXIS2_PLACEMENT_3D('',#38721,#14074,#14075);
#12094=AXIS2_PLACEMENT_3D('',#38722,#14076,#14077);
#12095=AXIS2_PLACEMENT_3D('',#38731,#14082,#14083);
#12096=AXIS2_PLACEMENT_3D('',#38737,#14087,#14088);
#12097=AXIS2_PLACEMENT_3D('',#38743,#14092,#14093);
#12098=AXIS2_PLACEMENT_3D('',#38749,#14097,#14098);
#12099=AXIS2_PLACEMENT_3D('',#38755,#14102,#14103);
#12100=AXIS2_PLACEMENT_3D('',#38758,#14106,#14107);
#12101=AXIS2_PLACEMENT_3D('',#38759,#14108,#14109);
#12102=AXIS2_PLACEMENT_3D('',#38761,#14110,#14111);
#12103=AXIS2_PLACEMENT_3D('',#38762,#14112,#14113);
#12104=AXIS2_PLACEMENT_3D('',#38765,#14115,#14116);
#12105=AXIS2_PLACEMENT_3D('',#38766,#14117,#14118);
#12106=AXIS2_PLACEMENT_3D('',#38767,#14119,#14120);
#13961=DIRECTION('axis',(0.,0.,1.));
#13962=DIRECTION('refdir',(1.,0.,0.));
#13963=DIRECTION('center_axis',(0.,0.,1.));
#13964=DIRECTION('ref_axis',(1.,0.,0.));
#13965=DIRECTION('',(0.,0.,-1.));
#13966=DIRECTION('center_axis',(0.,0.,-1.));
#13967=DIRECTION('ref_axis',(1.,0.,0.));
#13968=DIRECTION('center_axis',(0.,0.,1.));
#13969=DIRECTION('ref_axis',(1.,0.,0.));
#13970=DIRECTION('',(0.,0.,-1.));
#13971=DIRECTION('center_axis',(0.,0.,1.));
#13972=DIRECTION('ref_axis',(1.,0.,0.));
#13973=DIRECTION('',(0.,0.,-1.));
#13974=DIRECTION('center_axis',(0.,0.,1.));
#13975=DIRECTION('ref_axis',(1.,0.,0.));
#13976=DIRECTION('',(0.,0.,-1.));
#13977=DIRECTION('center_axis',(0.,0.,1.));
#13978=DIRECTION('ref_axis',(1.,0.,0.));
#13979=DIRECTION('',(0.,0.,-1.));
#13980=DIRECTION('center_axis',(0.,0.,1.));
#13981=DIRECTION('ref_axis',(1.,0.,0.));
#13982=DIRECTION('',(0.,0.,-1.));
#13983=DIRECTION('center_axis',(0.,0.,1.));
#13984=DIRECTION('ref_axis',(1.,0.,0.));
#13985=DIRECTION('',(0.,0.,-1.));
#13986=DIRECTION('center_axis',(0.,0.,1.));
#13987=DIRECTION('ref_axis',(1.,0.,0.));
#13988=DIRECTION('',(0.,0.,-1.));
#13989=DIRECTION('center_axis',(0.,0.,1.));
#13990=DIRECTION('ref_axis',(1.,0.,0.));
#13991=DIRECTION('',(0.,0.,-1.));
#13992=DIRECTION('center_axis',(0.,0.,1.));
#13993=DIRECTION('ref_axis',(1.,0.,0.));
#13994=DIRECTION('',(0.,0.,-1.));
#13995=DIRECTION('center_axis',(0.,0.,1.));
#13996=DIRECTION('ref_axis',(1.,0.,0.));
#13997=DIRECTION('',(0.,0.,-1.));
#13998=DIRECTION('center_axis',(0.,0.,1.));
#13999=DIRECTION('ref_axis',(1.,0.,0.));
#14000=DIRECTION('',(0.,0.,-1.));
#14001=DIRECTION('center_axis',(0.,0.,1.));
#14002=DIRECTION('ref_axis',(1.,0.,0.));
#14003=DIRECTION('',(0.,0.,-1.));
#14004=DIRECTION('center_axis',(0.,0.,1.));
#14005=DIRECTION('ref_axis',(1.,0.,0.));
#14006=DIRECTION('',(0.,0.,-1.));
#14007=DIRECTION('center_axis',(0.,0.,1.));
#14008=DIRECTION('ref_axis',(1.,0.,0.));
#14009=DIRECTION('',(0.,0.,-1.));
#14010=DIRECTION('center_axis',(0.,0.,1.));
#14011=DIRECTION('ref_axis',(1.,0.,0.));
#14012=DIRECTION('',(0.,0.,-1.));
#14013=DIRECTION('center_axis',(0.,0.,1.));
#14014=DIRECTION('ref_axis',(1.,1.29731060939901E-13,0.));
#14015=DIRECTION('',(0.,0.,1.));
#14016=DIRECTION('center_axis',(0.,0.,-1.));
#14017=DIRECTION('ref_axis',(1.,1.29731060939901E-13,0.));
#14018=DIRECTION('center_axis',(0.,0.,1.));
#14019=DIRECTION('ref_axis',(1.,1.29731060939901E-13,0.));
#14020=DIRECTION('',(0.,0.,1.));
#14021=DIRECTION('center_axis',(0.,0.,1.));
#14022=DIRECTION('ref_axis',(1.,1.29731060939901E-13,0.));
#14023=DIRECTION('',(0.,0.,1.));
#14024=DIRECTION('center_axis',(0.,0.,1.));
#14025=DIRECTION('ref_axis',(1.,1.29731060939901E-13,0.));
#14026=DIRECTION('',(0.,0.,1.));
#14027=DIRECTION('center_axis',(0.,0.,1.));
#14028=DIRECTION('ref_axis',(1.,1.29731060939901E-13,0.));
#14029=DIRECTION('',(0.,0.,1.));
#14030=DIRECTION('center_axis',(0.,0.,1.));
#14031=DIRECTION('ref_axis',(1.,1.29731060939901E-13,0.));
#14032=DIRECTION('',(0.,0.,1.));
#14033=DIRECTION('center_axis',(0.,0.,1.));
#14034=DIRECTION('ref_axis',(1.,1.29731060939901E-13,0.));
#14035=DIRECTION('',(0.,0.,1.));
#14036=DIRECTION('center_axis',(0.,0.,1.));
#14037=DIRECTION('ref_axis',(1.,1.29731060939901E-13,0.));
#14038=DIRECTION('',(0.,0.,1.));
#14039=DIRECTION('center_axis',(0.,0.,1.));
#14040=DIRECTION('ref_axis',(1.,1.29731060939901E-13,0.));
#14041=DIRECTION('',(0.,0.,1.));
#14042=DIRECTION('center_axis',(0.,0.,1.));
#14043=DIRECTION('ref_axis',(1.,1.29731060939901E-13,0.));
#14044=DIRECTION('',(0.,0.,1.));
#14045=DIRECTION('center_axis',(0.,0.,1.));
#14046=DIRECTION('ref_axis',(1.,1.29731060939901E-13,0.));
#14047=DIRECTION('',(0.,0.,1.));
#14048=DIRECTION('center_axis',(0.,0.,1.));
#14049=DIRECTION('ref_axis',(1.,1.29731060939901E-13,0.));
#14050=DIRECTION('',(0.,0.,1.));
#14051=DIRECTION('center_axis',(0.,0.,1.));
#14052=DIRECTION('ref_axis',(1.,1.29731060939901E-13,0.));
#14053=DIRECTION('',(0.,0.,1.));
#14054=DIRECTION('center_axis',(0.,0.,1.));
#14055=DIRECTION('ref_axis',(1.,1.29731060939901E-13,0.));
#14056=DIRECTION('',(0.,0.,1.));
#14057=DIRECTION('center_axis',(0.,0.,1.));
#14058=DIRECTION('ref_axis',(1.,1.29731060939901E-13,0.));
#14059=DIRECTION('',(0.,0.,1.));
#14060=DIRECTION('center_axis',(0.,0.,1.));
#14061=DIRECTION('ref_axis',(1.,1.29731060939901E-13,0.));
#14062=DIRECTION('',(0.,0.,1.));
#14063=DIRECTION('center_axis',(0.,0.,-1.));
#14064=DIRECTION('ref_axis',(1.,0.,0.));
#14065=DIRECTION('center_axis',(0.,0.,-1.));
#14066=DIRECTION('ref_axis',(1.,0.,0.));
#14067=DIRECTION('',(0.707106781186548,8.65956056235494E-17,0.707106781186547));
#14068=DIRECTION('center_axis',(0.,0.,1.));
#14069=DIRECTION('ref_axis',(1.,0.,0.));
#14070=DIRECTION('center_axis',(0.,0.,1.));
#14071=DIRECTION('ref_axis',(1.,1.29731060939901E-13,0.));
#14072=DIRECTION('center_axis',(0.,0.,-1.));
#14073=DIRECTION('ref_axis',(1.,1.29731060939901E-13,0.));
#14074=DIRECTION('center_axis',(0.,0.,1.));
#14075=DIRECTION('ref_axis',(1.,0.,0.));
#14076=DIRECTION('center_axis',(-1.60246890531964E-16,-1.,0.));
#14077=DIRECTION('ref_axis',(1.,-1.60246890531964E-16,0.));
#14078=DIRECTION('',(1.,-1.60246890531964E-16,0.));
#14079=DIRECTION('',(0.,0.,1.));
#14080=DIRECTION('',(1.,-1.60246890531964E-16,0.));
#14081=DIRECTION('',(0.,0.,1.));
#14082=DIRECTION('center_axis',(-0.866025403784439,-0.5,0.));
#14083=DIRECTION('ref_axis',(0.5,-0.866025403784439,0.));
#14084=DIRECTION('',(0.5,-0.866025403784439,0.));
#14085=DIRECTION('',(0.,0.,1.));
#14086=DIRECTION('',(0.5,-0.866025403784439,0.));
#14087=DIRECTION('center_axis',(-0.866025403784439,0.5,0.));
#14088=DIRECTION('ref_axis',(-0.5,-0.866025403784439,0.));
#14089=DIRECTION('',(-0.5,-0.866025403784439,0.));
#14090=DIRECTION('',(0.,0.,1.));
#14091=DIRECTION('',(-0.5,-0.866025403784439,0.));
#14092=DIRECTION('center_axis',(1.60246890531964E-16,1.,0.));
#14093=DIRECTION('ref_axis',(-1.,1.60246890531964E-16,0.));
#14094=DIRECTION('',(-1.,1.60246890531964E-16,0.));
#14095=DIRECTION('',(0.,0.,1.));
#14096=DIRECTION('',(-1.,1.60246890531964E-16,0.));
#14097=DIRECTION('center_axis',(0.866025403784439,0.5,0.));
#14098=DIRECTION('ref_axis',(-0.5,0.866025403784439,0.));
#14099=DIRECTION('',(-0.5,0.866025403784439,0.));
#14100=DIRECTION('',(0.,0.,1.));
#14101=DIRECTION('',(-0.5,0.866025403784439,0.));
#14102=DIRECTION('center_axis',(0.866025403784439,-0.5,0.));
#14103=DIRECTION('ref_axis',(0.5,0.866025403784439,0.));
#14104=DIRECTION('',(0.5,0.866025403784439,0.));
#14105=DIRECTION('',(0.5,0.866025403784439,0.));
#14106=DIRECTION('center_axis',(0.,0.,1.));
#14107=DIRECTION('ref_axis',(1.,0.,0.));
#14108=DIRECTION('center_axis',(0.,0.,1.));
#14109=DIRECTION('ref_axis',(1.,0.,0.));
#14110=DIRECTION('center_axis',(0.,0.,1.));
#14111=DIRECTION('ref_axis',(1.,0.,0.));
#14112=DIRECTION('center_axis',(0.,0.,1.));
#14113=DIRECTION('ref_axis',(1.,0.,0.));
#14114=DIRECTION('',(0.,0.,-1.));
#14115=DIRECTION('center_axis',(0.,0.,1.));
#14116=DIRECTION('ref_axis',(1.,0.,0.));
#14117=DIRECTION('center_axis',(0.,0.,1.));
#14118=DIRECTION('ref_axis',(1.,0.,0.));
#14119=DIRECTION('center_axis',(0.,0.,1.));
#14120=DIRECTION('ref_axis',(1.,0.,0.));
#36370=CARTESIAN_POINT('',(0.,0.,0.));
#36371=CARTESIAN_POINT('Origin',(0.,0.,0.));
#36372=CARTESIAN_POINT('',(-0.195633559071744,0.00012731057411345,0.0225869692124231));
#36373=CARTESIAN_POINT('',(-0.195587799559821,0.000207186393275607,0.0124130307875758));
#36374=CARTESIAN_POINT('',(-0.1954,-2.39295984553393E-17,0.));
#36375=CARTESIAN_POINT('',(0.0861525859670522,0.175382131162755,0.));
#36376=CARTESIAN_POINT('Ctrl Pts',(-0.195633559071744,0.00012731057411345,
0.0225869692124231));
#36377=CARTESIAN_POINT('Ctrl Pts',(-0.195680032440099,0.00682557629313676,
0.0222037301306047));
#36378=CARTESIAN_POINT('Ctrl Pts',(-0.195365903766855,0.0135191473590706,
0.0218204910487863));
#36379=CARTESIAN_POINT('Ctrl Pts',(-0.194676806606145,0.0201735328972743,
0.0214372519669679));
#36380=CARTESIAN_POINT('Ctrl Pts',(-0.188017193281744,0.0844832371344698,
0.01773353028412));
#36381=CARTESIAN_POINT('Ctrl Pts',(-0.146336311091822,0.145133095416213,
0.0140298086012721));
#36382=CARTESIAN_POINT('Ctrl Pts',(-0.0886884671668765,0.17445317403525,
0.0103260869184242));
#36383=CARTESIAN_POINT('Ctrl Pts',(-0.0351138290053491,0.201701592986141,
0.00688405794561611));
#36384=CARTESIAN_POINT('Ctrl Pts',(0.0322511385444639,0.201891139473935,
0.00344202897280807));
#36385=CARTESIAN_POINT('Ctrl Pts',(0.0863567639152679,0.175641488315944,
2.92734586571086E-18));
#36386=CARTESIAN_POINT('',(-0.0861525859670574,0.175382131162752,1.38777878078145E-17));
#36387=CARTESIAN_POINT('Origin',(0.,0.,0.));
#36388=CARTESIAN_POINT('Ctrl Pts',(-0.0861525859670571,0.175382131162752,
2.28983498828939E-16));
#36389=CARTESIAN_POINT('Ctrl Pts',(-0.144496782441851,0.146721837385109,
0.00370621399437224));
#36390=CARTESIAN_POINT('Ctrl Pts',(-0.18691020329229,0.0869083656944534,
0.00741242798874424));
#36391=CARTESIAN_POINT('Ctrl Pts',(-0.194380023116171,0.0227435527544788,
0.0111186419831163));
#36392=CARTESIAN_POINT('Ctrl Pts',(-0.195249630318745,0.0152737362394887,
0.0115501049179361));
#36393=CARTESIAN_POINT('Ctrl Pts',(-0.195645657185248,0.00774494727773659,
0.0119815678527559));
#36394=CARTESIAN_POINT('Ctrl Pts',(-0.195587799559821,0.000207186393275607,
0.0124130307875758));
#36395=CARTESIAN_POINT('Origin',(0.,0.,0.));
#36396=CARTESIAN_POINT('',(-0.195128203910989,9.79727872364722E-5,0.092586969212423));
#36397=CARTESIAN_POINT('',(-0.195118672945361,9.16100096969453E-5,0.0824130307875757));
#36398=CARTESIAN_POINT('',(-0.1954,-2.39295984553393E-17,0.));
#36399=CARTESIAN_POINT('Ctrl Pts',(-0.195128203910989,9.79727872364722E-5,
0.092586969212423));
#36400=CARTESIAN_POINT('Ctrl Pts',(-0.19524730612105,0.0263901717292074,
0.0910927268943587));
#36401=CARTESIAN_POINT('Ctrl Pts',(-0.190305141123492,0.0526394079969068,
0.0895984845762944));
#36402=CARTESIAN_POINT('Ctrl Pts',(-0.180089049647467,0.0766440059940591,
0.0881042422582301));
#36403=CARTESIAN_POINT('Ctrl Pts',(-0.154766811710363,0.136143291361155,
0.0844005205753822));
#36404=CARTESIAN_POINT('Ctrl Pts',(-0.0970428066964404,0.181852045762203,
0.0806967988925343));
#36405=CARTESIAN_POINT('Ctrl Pts',(-0.0333230591869142,0.192861999489257,
0.0769930772096863));
#36406=CARTESIAN_POINT('Ctrl Pts',(0.030396688322612,0.20387195321631,0.0732893555268384));
#36407=CARTESIAN_POINT('Ctrl Pts',(0.100112178327742,0.18018310626937,0.0695856338439906));
#36408=CARTESIAN_POINT('Ctrl Pts',(0.143930998255098,0.132629143144902,
0.0658819121611426));
#36409=CARTESIAN_POINT('Ctrl Pts',(0.187749818182454,0.0850751800204342,
0.0621781904782947));
#36410=CARTESIAN_POINT('Ctrl Pts',(0.205671968032037,0.0136561007184397,
0.0584744687954468));
#36411=CARTESIAN_POINT('Ctrl Pts',(0.189499805994521,-0.0489512382298273,
0.0547707471125989));
#36412=CARTESIAN_POINT('Ctrl Pts',(0.173327643957006,-0.111558577178094,
0.051067025429751));
#36413=CARTESIAN_POINT('Ctrl Pts',(0.123061170032392,-0.165354175772633,
0.0473633037469032));
#36414=CARTESIAN_POINT('Ctrl Pts',(0.0616932989107385,-0.18573955796291,
0.0436595820640553));
#36415=CARTESIAN_POINT('Ctrl Pts',(0.000325427789084558,-0.206124940153187,
0.0399558603812074));
#36416=CARTESIAN_POINT('Ctrl Pts',(-0.0721438405296094,-0.193100105939202,
0.0362521386983595));
#36417=CARTESIAN_POINT('Ctrl Pts',(-0.122559302459517,-0.152602913735885,
0.0325484170155115));
#36418=CARTESIAN_POINT('Ctrl Pts',(-0.167758072371516,-0.11629613001496,
0.029227934414482));
#36419=CARTESIAN_POINT('Ctrl Pts',(-0.195230901779331,-0.0579081973692791,
0.0259074518134526));
#36420=CARTESIAN_POINT('Ctrl Pts',(-0.195633559071744,0.00012731057411345,
0.0225869692124231));
#36421=CARTESIAN_POINT('Ctrl Pts',(-0.195587799559821,0.000207186393275607,
0.0124130307875758));
#36422=CARTESIAN_POINT('Ctrl Pts',(-0.195148667238412,-0.0570034995103637,
0.015687781847128));
#36423=CARTESIAN_POINT('Ctrl Pts',(-0.168562951923343,-0.114731024226281,
0.0189625329066803));
#36424=CARTESIAN_POINT('Ctrl Pts',(-0.12444215732779,-0.151113938431406,
0.0222372839662326));
#36425=CARTESIAN_POINT('Ctrl Pts',(-0.0745082529182101,-0.192290462488019,
0.0259434979606046));
#36426=CARTESIAN_POINT('Ctrl Pts',(-0.00211422530173012,-0.20612735641195,
0.0296497119549767));
#36427=CARTESIAN_POINT('Ctrl Pts',(0.0595334795120667,-0.186428772433344,
0.0333559259493488));
#36428=CARTESIAN_POINT('Ctrl Pts',(0.121181184325864,-0.166730188454737,
0.0370621399437209));
#36429=CARTESIAN_POINT('Ctrl Pts',(0.172082566336977,-0.113496126573593,
0.040768353938093));
#36430=CARTESIAN_POINT('Ctrl Pts',(0.18894870924304,-0.0510370283185346,
0.0444745679324651));
#36431=CARTESIAN_POINT('Ctrl Pts',(0.205814852149104,0.0114220699365238,
0.0481807819268372));
#36432=CARTESIAN_POINT('Ctrl Pts',(0.188645755950116,0.0831062045654966,
0.0518869959212093));
#36433=CARTESIAN_POINT('Ctrl Pts',(0.145292142815886,0.131145007703775,
0.0555932099155814));
#36434=CARTESIAN_POINT('Ctrl Pts',(0.101938529681656,0.179183810842053,
0.0592994239099535));
#36435=CARTESIAN_POINT('Ctrl Pts',(0.0324003996121834,0.203577282489637,
0.0630056379043256));
#36436=CARTESIAN_POINT('Ctrl Pts',(-0.0314654015224673,0.193172336479658,
0.0667118518986976));
#36437=CARTESIAN_POINT('Ctrl Pts',(-0.0953312026571179,0.18276739046968,
0.0704180658930697));
#36438=CARTESIAN_POINT('Ctrl Pts',(-0.153524674856946,0.137564026802139,
0.0741242798874417));
#36439=CARTESIAN_POINT('Ctrl Pts',(-0.179395555636014,0.0782560471576942,
0.0778304938818138));
#36440=CARTESIAN_POINT('Ctrl Pts',(-0.190058212652462,0.0538123240897563,
0.0793580061837345));
#36441=CARTESIAN_POINT('Ctrl Pts',(-0.195230335199157,0.0269726953471863,
0.0808855184856551));
#36442=CARTESIAN_POINT('Ctrl Pts',(-0.195118672945361,9.16100096969453E-5,
0.0824130307875757));
#36443=CARTESIAN_POINT('Origin',(0.,0.,0.));
#36444=CARTESIAN_POINT('',(-0.195279554503994,-0.000168121501241181,0.162586969212423));
#36445=CARTESIAN_POINT('',(-0.195287184048439,-0.0001702989282844,0.152413030787576));
#36446=CARTESIAN_POINT('',(-0.1954,-2.39295984553393E-17,0.));
#36447=CARTESIAN_POINT('Ctrl Pts',(-0.195279554503994,-0.000168121501241181,
0.162586969212423));
#36448=CARTESIAN_POINT('Ctrl Pts',(-0.194903656010943,0.0455834752155161,
0.159981723658113));
#36449=CARTESIAN_POINT('Ctrl Pts',(-0.178856730317397,0.091572573117829,
0.157376478103802));
#36450=CARTESIAN_POINT('Ctrl Pts',(-0.149500760249196,0.126316552728133,
0.154771232549492));
#36451=CARTESIAN_POINT('Ctrl Pts',(-0.107767134532898,0.175709989142681,
0.151067510866644));
#36452=CARTESIAN_POINT('Ctrl Pts',(-0.039135122029848,0.202376358702057,
0.147363789183796));
#36453=CARTESIAN_POINT('Ctrl Pts',(0.0249990333148566,0.194116955279127,
0.143660067500948));
#36454=CARTESIAN_POINT('Ctrl Pts',(0.0891331886595613,0.185857551856197,
0.139956345818101));
#36455=CARTESIAN_POINT('Ctrl Pts',(0.14876948684592,0.142672375450961,0.136252624135253));
#36456=CARTESIAN_POINT('Ctrl Pts',(0.176626827046517,0.0843167597229759,
0.132548902452405));
#36457=CARTESIAN_POINT('Ctrl Pts',(0.204484167247113,0.0259611439949913,
0.128845180769557));
#36458=CARTESIAN_POINT('Ctrl Pts',(0.200562549461947,-0.0475649110557425,
0.125141459086709));
#36459=CARTESIAN_POINT('Ctrl Pts',(0.166655969053473,-0.102626219289756,
0.121437737403861));
#36460=CARTESIAN_POINT('Ctrl Pts',(0.132749388644999,-0.157687527523771,
0.117734015721013));
#36461=CARTESIAN_POINT('Ctrl Pts',(0.0688578456132156,-0.194284088941065,
0.114030294038165));
#36462=CARTESIAN_POINT('Ctrl Pts',(0.00420898544956178,-0.19567474659654,
0.110326572355317));
#36463=CARTESIAN_POINT('Ctrl Pts',(-0.0604398747140919,-0.197065404252014,
0.106622850672469));
#36464=CARTESIAN_POINT('Ctrl Pts',(-0.125846052009616,-0.16325015814567,
0.102919128989622));
#36465=CARTESIAN_POINT('Ctrl Pts',(-0.162088905227235,-0.109697626925925,
0.0992154073067737));
#36466=CARTESIAN_POINT('Ctrl Pts',(-0.183709816073764,-0.0777505145902677,
0.0970059279419901));
#36467=CARTESIAN_POINT('Ctrl Pts',(-0.194952091996443,-0.0387793032173158,
0.0947964485772066));
#36468=CARTESIAN_POINT('Ctrl Pts',(-0.195128203910989,9.79727872364722E-5,
0.092586969212423));
#36469=CARTESIAN_POINT('Ctrl Pts',(-0.195118672945361,9.16100096969453E-5,
0.0824130307875757));
#36470=CARTESIAN_POINT('Ctrl Pts',(-0.194959408276249,-0.0382490737583375,
0.0845917324800272));
#36471=CARTESIAN_POINT('Ctrl Pts',(-0.184051065227066,-0.0766740948347571,
0.0867704341724787));
#36472=CARTESIAN_POINT('Ctrl Pts',(-0.162993550876047,-0.10835175828476,
0.0889491358649302));
#36473=CARTESIAN_POINT('Ctrl Pts',(-0.127172375978705,-0.162238988461419,
0.0926553498593023));
#36474=CARTESIAN_POINT('Ctrl Pts',(-0.0619817368257128,-0.196600853193387,
0.0963615638536743));
#36475=CARTESIAN_POINT('Ctrl Pts',(0.0027186436745272,-0.195701720127518,
0.100067777848046));
#36476=CARTESIAN_POINT('Ctrl Pts',(0.0674190241747668,-0.194802587061648,
0.103773991842418));
#36477=CARTESIAN_POINT('Ctrl Pts',(0.131629146022255,-0.15864245619794,
0.107480205836791));
#36478=CARTESIAN_POINT('Ctrl Pts',(0.165939903784035,-0.103781956343241,
0.111186419831163));
#36479=CARTESIAN_POINT('Ctrl Pts',(0.200250661545815,-0.0489214564885407,
0.114892633825535));
#36480=CARTESIAN_POINT('Ctrl Pts',(0.204662055221888,0.0246394123571516,
0.118598847819907));
#36481=CARTESIAN_POINT('Ctrl Pts',(0.177153295980734,0.0832073910176122,
0.122305061814279));
#36482=CARTESIAN_POINT('Ctrl Pts',(0.149644536739581,0.141775369678073,
0.126011275808651));
#36483=CARTESIAN_POINT('Ctrl Pts',(0.0902156245812001,0.185350458153303,
0.129717489803023));
#36484=CARTESIAN_POINT('Ctrl Pts',(0.0260864347694114,0.193974733338565,
0.133423703797395));
#36485=CARTESIAN_POINT('Ctrl Pts',(-0.0380427550423769,0.202599008523827,
0.137129917791767));
#36486=CARTESIAN_POINT('Ctrl Pts',(-0.106872222507573,0.176272470419122,
0.140836131786139));
#36487=CARTESIAN_POINT('Ctrl Pts',(-0.148876654315921,0.127053027794487,
0.144542345780511));
#36488=CARTESIAN_POINT('Ctrl Pts',(-0.178610829781436,0.0922114770268632,
0.147165907449533));
#36489=CARTESIAN_POINT('Ctrl Pts',(-0.194903067523895,0.0458983666015645,
0.149789469118554));
#36490=CARTESIAN_POINT('Ctrl Pts',(-0.195287184048439,-0.0001702989282844,
0.152413030787576));
#36491=CARTESIAN_POINT('Origin',(0.,0.,0.));
#36492=CARTESIAN_POINT('',(-0.19571996697324,4.08272333451705E-6,0.232586969212423));
#36493=CARTESIAN_POINT('',(-0.195720915199432,4.37834080700025E-6,0.222413030787575));
#36494=CARTESIAN_POINT('',(-0.1954,-2.39295984553393E-17,0.));
#36495=CARTESIAN_POINT('Ctrl Pts',(-0.19571996697324,4.08272333451705E-6,
0.232586969212423));
#36496=CARTESIAN_POINT('Ctrl Pts',(-0.19573993069631,0.0648866965015804,
0.228870720421867));
#36497=CARTESIAN_POINT('Ctrl Pts',(-0.160252793092098,0.129750264469882,
0.225154471631311));
#36498=CARTESIAN_POINT('Ctrl Pts',(-0.105631192010051,0.164767712566922,
0.221438222840754));
#36499=CARTESIAN_POINT('Ctrl Pts',(-0.0511937149515876,0.19966712030426,
0.217734501157906));
#36500=CARTESIAN_POINT('Ctrl Pts',(0.0222490761444335,0.204921286910345,
0.214030779475058));
#36501=CARTESIAN_POINT('Ctrl Pts',(0.0811002035332165,0.178126653559889,
0.210327057792211));
#36502=CARTESIAN_POINT('Ctrl Pts',(0.139951330921999,0.151332020209433,
0.206623336109363));
#36503=CARTESIAN_POINT('Ctrl Pts',(0.184210794603544,0.0924885869024359,
0.202919614426515));
#36504=CARTESIAN_POINT('Ctrl Pts',(0.193631757329266,0.028514740055385,
0.199215892743667));
#36505=CARTESIAN_POINT('Ctrl Pts',(0.203052720054988,-0.0354591067916664,
0.195512171060819));
#36506=CARTESIAN_POINT('Ctrl Pts',(0.177635181824887,-0.104563367178771,
0.191808449377971));
#36507=CARTESIAN_POINT('Ctrl Pts',(0.129006594271768,-0.147185755477259,
0.188104727695123));
#36508=CARTESIAN_POINT('Ctrl Pts',(0.0803780067186484,-0.189808143775746,
0.184401006012275));
#36509=CARTESIAN_POINT('Ctrl Pts',(0.00853836984250916,-0.205948659985616,
0.180697284329427));
#36510=CARTESIAN_POINT('Ctrl Pts',(-0.0536487147273854,-0.188223703762279,
0.176993562646579));
#36511=CARTESIAN_POINT('Ctrl Pts',(-0.11583579929728,-0.170498747538942,
0.173289840963732));
#36512=CARTESIAN_POINT('Ctrl Pts',(-0.168370331560931,-0.118908318882399,
0.169586119280884));
#36513=CARTESIAN_POINT('Ctrl Pts',(-0.187219978227984,-0.0570528529192665,
0.165882397598036));
#36514=CARTESIAN_POINT('Ctrl Pts',(-0.192810540551016,-0.0387073187246384,
0.164783921469498));
#36515=CARTESIAN_POINT('Ctrl Pts',(-0.195438048401311,-0.0194588316428207,
0.163685445340961));
#36516=CARTESIAN_POINT('Ctrl Pts',(-0.195279554503994,-0.000168121501241181,
0.162586969212423));
#36517=CARTESIAN_POINT('Ctrl Pts',(-0.195287184048439,-0.0001702989282844,
0.152413030787576));
#36518=CARTESIAN_POINT('Ctrl Pts',(-0.195445695530526,-0.0191812291650776,
0.153495683112926));
#36519=CARTESIAN_POINT('Ctrl Pts',(-0.192895173588402,-0.0381505322742495,
0.154578335438277));
#36520=CARTESIAN_POINT('Ctrl Pts',(-0.187462310228399,-0.0562548805321496,
0.155660987763628));
#36521=CARTESIAN_POINT('Ctrl Pts',(-0.168864138181028,-0.118230999089587,
0.159367201758));
#36522=CARTESIAN_POINT('Ctrl Pts',(-0.116488397934787,-0.170070889059896,
0.163073415752372));
#36523=CARTESIAN_POINT('Ctrl Pts',(-0.0543243355780667,-0.188030816136644,
0.166779629746744));
#36524=CARTESIAN_POINT('Ctrl Pts',(0.0078397267786532,-0.205990743213392,
0.170485843741116));
#36525=CARTESIAN_POINT('Ctrl Pts',(0.0797921112458524,-0.190070707396579,
0.174192057735488));
#36526=CARTESIAN_POINT('Ctrl Pts',(0.128577075941843,-0.147562399010748,
0.17789827172986));
#36527=CARTESIAN_POINT('Ctrl Pts',(0.177362040637834,-0.105054090624917,
0.181604485724232));
#36528=CARTESIAN_POINT('Ctrl Pts',(0.202979585562615,-0.0359575096700667,
0.185310699718604));
#36529=CARTESIAN_POINT('Ctrl Pts',(0.193696313672928,0.028079594435252,
0.189016913712976));
#36530=CARTESIAN_POINT('Ctrl Pts',(0.184413041783241,0.0921166985405712,
0.192723127707349));
#36531=CARTESIAN_POINT('Ctrl Pts',(0.140228953079084,0.151094325796358,
0.196429341701721));
#36532=CARTESIAN_POINT('Ctrl Pts',(0.0813813216582781,0.177999452248681,
0.200135555696093));
#36533=CARTESIAN_POINT('Ctrl Pts',(0.0225336902374724,0.204904578701004,
0.203841769690465));
#36534=CARTESIAN_POINT('Ctrl Pts',(-0.0509774838999832,0.199737204349863,
0.207547983684837));
#36535=CARTESIAN_POINT('Ctrl Pts',(-0.105482489992153,0.164864094185095,
0.211254197679209));
#36536=CARTESIAN_POINT('Ctrl Pts',(-0.16018451812442,0.129864926401004,
0.214973808715331));
#36537=CARTESIAN_POINT('Ctrl Pts',(-0.195742302622205,0.0649448754401196,
0.218693419751453));
#36538=CARTESIAN_POINT('Ctrl Pts',(-0.195720915199432,4.37834080700025E-6,
0.222413030787575));
#36539=CARTESIAN_POINT('Origin',(0.,0.,0.));
#36540=CARTESIAN_POINT('',(-0.195267691385146,0.000165493661177622,0.302586969212423));
#36541=CARTESIAN_POINT('',(-0.195274315056508,0.000167675988910205,0.292413030787576));
#36542=CARTESIAN_POINT('',(-0.1954,-2.39295984553393E-17,0.));
#36543=CARTESIAN_POINT('Ctrl Pts',(-0.195267691385146,0.000165493661177622,
0.302586969212423));
#36544=CARTESIAN_POINT('Ctrl Pts',(-0.195426560914452,0.0198992208020636,
0.301463438868469));
#36545=CARTESIAN_POINT('Ctrl Pts',(-0.192675342506316,0.0395896803504792,
0.300339908524515));
#36546=CARTESIAN_POINT('Ctrl Pts',(-0.186830808103941,0.0583146374609883,
0.29921637818056));
#36547=CARTESIAN_POINT('Ctrl Pts',(-0.167564280138135,0.120041523640586,
0.295512656497712));
#36548=CARTESIAN_POINT('Ctrl Pts',(-0.114682887836242,0.171276357431471,
0.291808934814864));
#36549=CARTESIAN_POINT('Ctrl Pts',(-0.0523776367443795,0.188581364320311,
0.288105213132016));
#36550=CARTESIAN_POINT('Ctrl Pts',(0.00992761434748341,0.20588637120915,
0.284401491449168));
#36551=CARTESIAN_POINT('Ctrl Pts',(0.0816567242293159,0.189261551195942,
0.280697769766321));
#36552=CARTESIAN_POINT('Ctrl Pts',(0.129996651882171,0.146312057934516,
0.276994048083473));
#36553=CARTESIAN_POINT('Ctrl Pts',(0.178336579535026,0.103362564673089,
0.273290326400625));
#36554=CARTESIAN_POINT('Ctrl Pts',(0.203287324958903,0.0340883981634439,
0.269586604717777));
#36555=CARTESIAN_POINT('Ctrl Pts',(0.193434974962867,-0.0298204336020968,
0.265882883034929));
#36556=CARTESIAN_POINT('Ctrl Pts',(0.183582624966831,-0.0937292653676373,
0.262179161352081));
#36557=CARTESIAN_POINT('Ctrl Pts',(0.138927179550881,-0.152272762389073,
0.258475439669233));
#36558=CARTESIAN_POINT('Ctrl Pts',(0.0798966206784796,-0.178669745083631,
0.254771717986385));
#36559=CARTESIAN_POINT('Ctrl Pts',(0.0208660618060775,-0.205066727778188,
0.251067996303538));
#36560=CARTESIAN_POINT('Ctrl Pts',(-0.0525396105227766,-0.199317196145866,
0.24736427462069));
#36561=CARTESIAN_POINT('Ctrl Pts',(-0.10674039873032,-0.16405131839538,
0.243660552937842));
#36562=CARTESIAN_POINT('Ctrl Pts',(-0.160757863467609,-0.128904720517098,
0.239969358362702));
#36563=CARTESIAN_POINT('Ctrl Pts',(-0.195700137841649,-0.0644411052866131,
0.236278163787563));
#36564=CARTESIAN_POINT('Ctrl Pts',(-0.19571996697324,4.08272333451705E-6,
0.232586969212423));
#36565=CARTESIAN_POINT('Ctrl Pts',(-0.195720915199432,4.37834080700025E-6,
0.222413030787575));
#36566=CARTESIAN_POINT('Ctrl Pts',(-0.195699681840184,-0.0644683222376,
0.226105847740198));
#36567=CARTESIAN_POINT('Ctrl Pts',(-0.160725113883781,-0.128960760246236,
0.22979866469282));
#36568=CARTESIAN_POINT('Ctrl Pts',(-0.106669244200308,-0.164098742623895,
0.233491481645442));
#36569=CARTESIAN_POINT('Ctrl Pts',(-0.0524172671136578,-0.199364200861572,
0.237197695639814));
#36570=CARTESIAN_POINT('Ctrl Pts',(0.0210547116140745,-0.205061829112049,
0.240903909634186));
#36571=CARTESIAN_POINT('Ctrl Pts',(0.0800949322066953,-0.178581989384044,
0.244610123628558));
#36572=CARTESIAN_POINT('Ctrl Pts',(0.139135152799316,-0.152102149656038,
0.24831633762293));
#36573=CARTESIAN_POINT('Ctrl Pts',(0.183743615256826,-0.0934448419495488,
0.252022551617302));
#36574=CARTESIAN_POINT('Ctrl Pts',(0.193488676008295,-0.0294763859316313,
0.255728765611674));
#36575=CARTESIAN_POINT('Ctrl Pts',(0.203233736759764,0.0344920700862864,
0.259434979606046));
#36576=CARTESIAN_POINT('Ctrl Pts',(0.178115395805193,0.103771674415633,
0.263141193600418));
#36577=CARTESIAN_POINT('Ctrl Pts',(0.129638398231036,0.146630865646616,
0.26684740759479));
#36578=CARTESIAN_POINT('Ctrl Pts',(0.0811614006568792,0.1894900568776,0.270553621589162));
#36579=CARTESIAN_POINT('Ctrl Pts',(0.00932574646313782,0.205928835010221,
0.274259835583535));
#36580=CARTESIAN_POINT('Ctrl Pts',(-0.0529662765081927,0.188417882975093,
0.277966049577907));
#36581=CARTESIAN_POINT('Ctrl Pts',(-0.115258299479523,0.170906930939964,
0.281672263572279));
#36582=CARTESIAN_POINT('Ctrl Pts',(-0.168006691228442,0.119446248737086,
0.285378477566651));
#36583=CARTESIAN_POINT('Ctrl Pts',(-0.187051544101399,0.0576059451476712,
0.289084691561023));
#36584=CARTESIAN_POINT('Ctrl Pts',(-0.192752575844056,0.0390941962730205,
0.290194137969874));
#36585=CARTESIAN_POINT('Ctrl Pts',(-0.195433466869055,0.0196523398123763,
0.291303584378725));
#36586=CARTESIAN_POINT('Ctrl Pts',(-0.195274315056508,0.000167675988910205,
0.292413030787576));
#36587=CARTESIAN_POINT('Origin',(0.,0.,0.));
#36588=CARTESIAN_POINT('',(-0.195135107115213,-0.000103745302926256,0.372586969212423));
#36589=CARTESIAN_POINT('',(-0.195125983814034,-9.67513988672578E-5,0.362413030787576));
#36590=CARTESIAN_POINT('',(-0.1954,-2.39295984553393E-17,0.));
#36591=CARTESIAN_POINT('Ctrl Pts',(-0.195135107115213,-0.000103745302926256,
0.372586969212423));
#36592=CARTESIAN_POINT('Ctrl Pts',(-0.19494564270682,0.0392108141373472,
0.370352435632223));
#36593=CARTESIAN_POINT('Ctrl Pts',(-0.183428685915158,0.078627490539017,
0.368117902052023));
#36594=CARTESIAN_POINT('Ctrl Pts',(-0.161345116677478,0.110788542383069,
0.365883368471823));
#36595=CARTESIAN_POINT('Ctrl Pts',(-0.124741775852795,0.164095230684139,
0.362179646788975));
#36596=CARTESIAN_POINT('Ctrl Pts',(-0.0591089924893776,0.197468687095231,
0.358475925106126));
#36597=CARTESIAN_POINT('Ctrl Pts',(0.00552900452708404,0.195641963566092,
0.354772203423278));
#36598=CARTESIAN_POINT('Ctrl Pts',(0.0701670015435453,0.193815240036952,
0.351068481740431));
#36599=CARTESIAN_POINT('Ctrl Pts',(0.13381021221305,0.156788336567581,0.347364760057583));
#36600=CARTESIAN_POINT('Ctrl Pts',(0.16734455320356,0.101499499073225,0.343661038374735));
#36601=CARTESIAN_POINT('Ctrl Pts',(0.20087889419407,0.0462106615788698,
0.339957316691887));
#36602=CARTESIAN_POINT('Ctrl Pts',(0.204304365505584,-0.0273401099404705,
0.336253595009039));
#36603=CARTESIAN_POINT('Ctrl Pts',(0.176053958557416,-0.0855064411333041,
0.332549873326191));
#36604=CARTESIAN_POINT('Ctrl Pts',(0.147803551609248,-0.143672772326139,
0.328846151643343));
#36605=CARTESIAN_POINT('Ctrl Pts',(0.0878772664013962,-0.186454663192466,
0.325142429960495));
#36606=CARTESIAN_POINT('Ctrl Pts',(0.0236888497103484,-0.194281203925035,
0.321438708277648));
#36607=CARTESIAN_POINT('Ctrl Pts',(-0.0404995669806982,-0.202107744657604,
0.3177349865948));
#36608=CARTESIAN_POINT('Ctrl Pts',(-0.108950115154941,-0.174978935256416,
0.314031264911952));
#36609=CARTESIAN_POINT('Ctrl Pts',(-0.150349557427203,-0.125305061271667,
0.310327543229104));
#36610=CARTESIAN_POINT('Ctrl Pts',(-0.179190407667273,-0.0906998424134863,
0.30774735189021));
#36611=CARTESIAN_POINT('Ctrl Pts',(-0.194902846959061,-0.0451530792879088,
0.305167160551317));
#36612=CARTESIAN_POINT('Ctrl Pts',(-0.195267691385146,0.000165493661177622,
0.302586969212423));
#36613=CARTESIAN_POINT('Ctrl Pts',(-0.195274315056508,0.000167675988910205,
0.292413030787576));
#36614=CARTESIAN_POINT('Ctrl Pts',(-0.194901804708373,-0.045438081105706,
0.295009798373097));
#36615=CARTESIAN_POINT('Ctrl Pts',(-0.178970412039892,-0.0912783539307832,
0.297606565958618));
#36616=CARTESIAN_POINT('Ctrl Pts',(-0.149789482266332,-0.125975537577289,
0.300203333544139));
#36617=CARTESIAN_POINT('Ctrl Pts',(-0.108141253561316,-0.175496791736879,
0.303909547538511));
#36618=CARTESIAN_POINT('Ctrl Pts',(-0.03950348215429,-0.202319375080107,
0.307615761532883));
#36619=CARTESIAN_POINT('Ctrl Pts',(0.0246862437687336,-0.194157962588032,
0.311321975527255));
#36620=CARTESIAN_POINT('Ctrl Pts',(0.0888759696917571,-0.185996550095957,
0.315028189521628));
#36621=CARTESIAN_POINT('Ctrl Pts',(0.148617650130778,-0.14285114176858,
0.318734403516));
#36622=CARTESIAN_POINT('Ctrl Pts',(0.176548299529208,-0.084483270534745,
0.322440617510372));
#36623=CARTESIAN_POINT('Ctrl Pts',(0.204478948927638,-0.0261153993009101,
0.326146831504744));
#36624=CARTESIAN_POINT('Ctrl Pts',(0.200598567285476,0.0474749348393822,
0.329853045499116));
#36625=CARTESIAN_POINT('Ctrl Pts',(0.166684453569178,0.102581762536563,
0.333559259493488));
#36626=CARTESIAN_POINT('Ctrl Pts',(0.13277033985288,0.157688590233743,0.33726547348786));
#36627=CARTESIAN_POINT('Ctrl Pts',(0.0688224940624468,0.194311911487812,
0.340971687482232));
#36628=CARTESIAN_POINT('Ctrl Pts',(0.00413041672205065,0.195677450731496,
0.344677901476604));
#36629=CARTESIAN_POINT('Ctrl Pts',(-0.0605616606183457,0.19704298997518,
0.348384115470976));
#36630=CARTESIAN_POINT('Ctrl Pts',(-0.125997969508704,0.163150747208479,
0.352090329465349));
#36631=CARTESIAN_POINT('Ctrl Pts',(-0.162207261036362,0.109524104808107,
0.355796543459721));
#36632=CARTESIAN_POINT('Ctrl Pts',(-0.183754705311226,0.0776119342016343,
0.358002039235672));
#36633=CARTESIAN_POINT('Ctrl Pts',(-0.194952253842872,0.0387114015523011,
0.360207535011624));
#36634=CARTESIAN_POINT('Ctrl Pts',(-0.195125983814034,-9.67513988672578E-5,
0.362413030787576));
#36635=CARTESIAN_POINT('Origin',(0.,0.,0.));
#36636=CARTESIAN_POINT('',(-0.195645574651684,-0.000107576288577632,0.442586969212423));
#36637=CARTESIAN_POINT('',(-0.195628130950281,-0.000119277919923279,0.432413030787576));
#36638=CARTESIAN_POINT('',(-0.1954,-2.39295984553393E-17,0.));
#36639=CARTESIAN_POINT('Ctrl Pts',(-0.195645574651684,-0.000107576288577632,
0.442586969212423));
#36640=CARTESIAN_POINT('Ctrl Pts',(-0.195258201164419,0.0583617837825317,
0.439241432395977));
#36641=CARTESIAN_POINT('Ctrl Pts',(-0.167312331125722,0.117152394520949,
0.435895895579531));
#36642=CARTESIAN_POINT('Ctrl Pts',(-0.121525966387556,0.153420296221226,
0.432550358763085));
#36643=CARTESIAN_POINT('Ctrl Pts',(-0.070837553387317,0.193571166257503,
0.428846637080237));
#36644=CARTESIAN_POINT('Ctrl Pts',(0.00171598407939347,0.206118438706562,
0.425142915397389));
#36645=CARTESIAN_POINT('Ctrl Pts',(0.0629444641593513,0.18532226587955,
0.421439193714541));
#36646=CARTESIAN_POINT('Ctrl Pts',(0.124172944239309,0.164526093052537,
0.417735472031693));
#36647=CARTESIAN_POINT('Ctrl Pts',(0.174076366932515,0.110386474949453,
0.414031750348845));
#36648=CARTESIAN_POINT('Ctrl Pts',(0.189826022128925,0.0476700023258525,
0.410328028665997));
#36649=CARTESIAN_POINT('Ctrl Pts',(0.205575677325334,-0.0150464702977478,
0.406624306983149));
#36650=CARTESIAN_POINT('Ctrl Pts',(0.187171565024948,-0.086339797441863,
0.402920585300301));
#36651=CARTESIAN_POINT('Ctrl Pts',(0.143032790007833,-0.133596290298842,
0.399216863617453));
#36652=CARTESIAN_POINT('Ctrl Pts',(0.0988940149907184,-0.180852783155821,
0.395513141934605));
#36653=CARTESIAN_POINT('Ctrl Pts',(0.0290205772568748,-0.204072441725662,
0.391809420251758));
#36654=CARTESIAN_POINT('Ctrl Pts',(-0.0346233738762281,-0.192633252011348,
0.38810569856891));
#36655=CARTESIAN_POINT('Ctrl Pts',(-0.0982673250093302,-0.181194062297035,
0.384401976886062));
#36656=CARTESIAN_POINT('Ctrl Pts',(-0.155681789541692,-0.135096024298568,
0.380698255203214));
#36657=CARTESIAN_POINT('Ctrl Pts',(-0.1806020726649,-0.0754270452038098,
0.376994533520366));
#36658=CARTESIAN_POINT('Ctrl Pts',(-0.190487422217158,-0.0517576224744695,
0.375525345417718));
#36659=CARTESIAN_POINT('Ctrl Pts',(-0.19525967846073,-0.0259527562563923,
0.374056157315071));
#36660=CARTESIAN_POINT('Ctrl Pts',(-0.195135107115213,-0.000103745302926256,
0.372586969212423));
#36661=CARTESIAN_POINT('Ctrl Pts',(-0.195125983814034,-9.67513988672578E-5,
0.362413030787576));
#36662=CARTESIAN_POINT('Ctrl Pts',(-0.195244197476311,-0.0265035587897937,
0.363913749005996));
#36663=CARTESIAN_POINT('Ctrl Pts',(-0.190258326051973,-0.0528675939020291,
0.365414467224416));
#36664=CARTESIAN_POINT('Ctrl Pts',(-0.1799560505048,-0.0769580726996389,
0.366915185442837));
#36665=CARTESIAN_POINT('Ctrl Pts',(-0.154513274280624,-0.136452565772967,
0.370621399437209));
#36666=CARTESIAN_POINT('Ctrl Pts',(-0.0966454476673152,-0.18208050988558,
0.374327613431581));
#36667=CARTESIAN_POINT('Ctrl Pts',(-0.0328572905191125,-0.192943316874967,
0.378033827425953));
#36668=CARTESIAN_POINT('Ctrl Pts',(0.0309308666290907,-0.203806123864353,
0.381740041420325));
#36669=CARTESIAN_POINT('Ctrl Pts',(0.100639354312189,-0.179903793730513,
0.385446255414697));
#36670=CARTESIAN_POINT('Ctrl Pts',(0.144340173058911,-0.132184112162819,
0.389152469409069));
#36671=CARTESIAN_POINT('Ctrl Pts',(0.188040991805633,-0.0844644305951239,
0.392858683403441));
#36672=CARTESIAN_POINT('Ctrl Pts',(0.205734141615979,-0.0129273975935752,
0.396564897397814));
#36673=CARTESIAN_POINT('Ctrl Pts',(0.189315776078089,0.0496614739501458,
0.400271111392186));
#36674=CARTESIAN_POINT('Ctrl Pts',(0.172897410540198,0.112250345493866,
0.403977325386558));
#36675=CARTESIAN_POINT('Ctrl Pts',(0.122367529654071,0.165891055579759,
0.40768353938093));
#36676=CARTESIAN_POINT('Ctrl Pts',(0.0608699149567017,0.186014995417357,
0.411389753375302));
#36677=CARTESIAN_POINT('Ctrl Pts',(-0.000627699740667481,0.206138935254955,
0.415095967369674));
#36678=CARTESIAN_POINT('Ctrl Pts',(-0.0730930482492791,0.19274610484426,
0.418802181364046));
#36679=CARTESIAN_POINT('Ctrl Pts',(-0.123335429038162,0.151970711029871,
0.422508395358418));
#36680=CARTESIAN_POINT('Ctrl Pts',(-0.168092015819396,0.115647443240051,
0.425809940501471));
#36681=CARTESIAN_POINT('Ctrl Pts',(-0.195213599025838,0.0575947822566119,
0.429111485644523));
#36682=CARTESIAN_POINT('Ctrl Pts',(-0.195628130950281,-0.000119277919923279,
0.432413030787576));
#36683=CARTESIAN_POINT('Origin',(0.,0.,0.));
#36684=CARTESIAN_POINT('',(-0.195458266482996,0.000173443779922018,0.512586969212423));
#36685=CARTESIAN_POINT('',(-0.195491180920002,0.000168629508682236,0.502413030787576));
#36686=CARTESIAN_POINT('',(-0.1954,-2.39295984553393E-17,0.));
#36687=CARTESIAN_POINT('Ctrl Pts',(-0.195458266482996,0.000173443779922018,
0.512586969212423));
#36688=CARTESIAN_POINT('Ctrl Pts',(-0.195579683437623,0.013363129532035,
0.511834150842579));
#36689=CARTESIAN_POINT('Ctrl Pts',(-0.194358523444966,0.0265304620125551,
0.511081332472735));
#36690=CARTESIAN_POINT('Ctrl Pts',(-0.191712292268468,0.0394048828472761,
0.510328514102891));
#36691=CARTESIAN_POINT('Ctrl Pts',(-0.178693343503641,0.10274455880328,
0.506624792420043));
#36692=CARTESIAN_POINT('Ctrl Pts',(-0.131181246839585,0.158994452273665,
0.502921070737195));
#36693=CARTESIAN_POINT('Ctrl Pts',(-0.0709107816346671,0.18242261056952,
0.499217349054347));
#36694=CARTESIAN_POINT('Ctrl Pts',(-0.0106403164297495,0.205850768865374,
0.495513627371499));
#36695=CARTESIAN_POINT('Ctrl Pts',(0.0623885173160298,0.196457191986698,
0.491809905688651));
#36696=CARTESIAN_POINT('Ctrl Pts',(0.114768109757825,0.158539044975217,
0.488106184005803));
#36697=CARTESIAN_POINT('Ctrl Pts',(0.167147702199619,0.120620897963737,
0.484402462322955));
#36698=CARTESIAN_POINT('Ctrl Pts',(0.19887805333743,0.0541781808194522,
0.480698740640107));
#36699=CARTESIAN_POINT('Ctrl Pts',(0.195443866449662,-0.0103943670439598,
0.476995018957259));
#36700=CARTESIAN_POINT('Ctrl Pts',(0.192009679561895,-0.0749669149073727,
0.473291297274411));
#36701=CARTESIAN_POINT('Ctrl Pts',(0.153410954648549,-0.137669293489913,
0.469587575591563));
#36702=CARTESIAN_POINT('Ctrl Pts',(0.0973049796091196,-0.169817810439032,
0.465883853908716));
#36703=CARTESIAN_POINT('Ctrl Pts',(0.0411990045696909,-0.20196632738815,
0.462180132225868));
#36704=CARTESIAN_POINT('Ctrl Pts',(-0.0324142205958206,-0.203560982703848,
0.45847641054302));
#36705=CARTESIAN_POINT('Ctrl Pts',(-0.0898597516275757,-0.17387228886878,
0.454772688860172));
#36706=CARTESIAN_POINT('Ctrl Pts',(-0.147305282659331,-0.144183595033712,
0.451068967177324));
#36707=CARTESIAN_POINT('Ctrl Pts',(-0.18858311955733,-0.0832115520478776,
0.447365245494476));
#36708=CARTESIAN_POINT('Ctrl Pts',(-0.194810393739446,-0.0188482967432128,
0.443661523811628));
#36709=CARTESIAN_POINT('Ctrl Pts',(-0.19541262996613,-0.0126237620787308,
0.443303338945226));
#36710=CARTESIAN_POINT('Ctrl Pts',(-0.195687048211354,-0.00636751036633503,
0.442945154078825));
#36711=CARTESIAN_POINT('Ctrl Pts',(-0.195645574651684,-0.000107576288577632,
0.442586969212423));
#36712=CARTESIAN_POINT('Ctrl Pts',(-0.195628130950281,-0.000119277919923279,
0.432413030787576));
#36713=CARTESIAN_POINT('Ctrl Pts',(-0.195678939935296,-0.00719326340995119,
0.432817699638895));
#36714=CARTESIAN_POINT('Ctrl Pts',(-0.195328521122814,-0.014262162001596,
0.433222368490215));
#36715=CARTESIAN_POINT('Ctrl Pts',(-0.194560169264522,-0.0212853377401693,
0.433627037341534));
#36716=CARTESIAN_POINT('Ctrl Pts',(-0.187523115632842,-0.0856080354777335,
0.437333251335906));
#36717=CARTESIAN_POINT('Ctrl Pts',(-0.145429595300328,-0.146095473734778,
0.441039465330279));
#36718=CARTESIAN_POINT('Ctrl Pts',(-0.0875593536694013,-0.175043093699665,
0.444745679324651));
#36719=CARTESIAN_POINT('Ctrl Pts',(-0.0296891120384743,-0.203990713664554,
0.448451893319023));
#36720=CARTESIAN_POINT('Ctrl Pts',(0.0439578508908652,-0.201398515337285,
0.452158107313395));
#36721=CARTESIAN_POINT('Ctrl Pts',(0.09964962855145,-0.168453781781564,
0.455864321307767));
#36722=CARTESIAN_POINT('Ctrl Pts',(0.155341406212034,-0.135509048225843,
0.459570535302139));
#36723=CARTESIAN_POINT('Ctrl Pts',(0.193077998603865,-0.072211779441669,
0.463276749296511));
#36724=CARTESIAN_POINT('Ctrl Pts',(0.195575227831571,-0.00755349757277263,
0.466982963290883));
#36725=CARTESIAN_POINT('Ctrl Pts',(0.198072457059277,0.0571047842961237,
0.470689177285256));
#36726=CARTESIAN_POINT('Ctrl Pts',(0.16533032312286,0.123124079249743,0.474395391279627));
#36727=CARTESIAN_POINT('Ctrl Pts',(0.112345433605614,0.160266118112717,
0.478101605273999));
#36728=CARTESIAN_POINT('Ctrl Pts',(0.059360544088369,0.197408156975691,
0.481807819268371));
#36729=CARTESIAN_POINT('Ctrl Pts',(-0.0138671010097046,0.20567293974802,
0.485514033262744));
#36730=CARTESIAN_POINT('Ctrl Pts',(-0.0737976517839776,0.181275016640803,
0.489220247257116));
#36731=CARTESIAN_POINT('Ctrl Pts',(-0.133728202558251,0.156877093533586,
0.492926461251488));
#36732=CARTESIAN_POINT('Ctrl Pts',(-0.180361659008724,0.0998164645468222,
0.49663267524586));
#36733=CARTESIAN_POINT('Ctrl Pts',(-0.192338886510923,0.0362281355122108,
0.500338889240232));
#36734=CARTESIAN_POINT('Ctrl Pts',(-0.194573194011967,0.0243659678682544,
0.501030269756014));
#36735=CARTESIAN_POINT('Ctrl Pts',(-0.195601481281436,0.0122766393772507,
0.501721650271795));
#36736=CARTESIAN_POINT('Ctrl Pts',(-0.195491180920002,0.000168629508682236,
0.502413030787576));
#36737=CARTESIAN_POINT('Origin',(0.,0.,0.));
#36738=CARTESIAN_POINT('',(-0.19507978584999,-3.45334863967226E-6,0.582586969212423));
#36739=CARTESIAN_POINT('',(-0.195080468396925,1.8981806121043E-5,0.572413030787576));
#36740=CARTESIAN_POINT('',(-0.1954,-2.39295984553393E-17,0.));
#36741=CARTESIAN_POINT('Ctrl Pts',(-0.195079815420139,-3.45302974047446E-6,
0.582586969212423));
#36742=CARTESIAN_POINT('Ctrl Pts',(-0.195074640707532,0.0328120037045956,
0.580723147606333));
#36743=CARTESIAN_POINT('Ctrl Pts',(-0.187237758907749,0.0656297824114404,
0.578859326000243));
#36744=CARTESIAN_POINT('Ctrl Pts',(-0.1715829951129,0.0941574404236039,
0.576995504394152));
#36745=CARTESIAN_POINT('Ctrl Pts',(-0.14047439120071,0.150846613462089,
0.573291782711304));
#36746=CARTESIAN_POINT('Ctrl Pts',(-0.0784943311216198,0.190594846094957,
0.569588061028457));
#36747=CARTESIAN_POINT('Ctrl Pts',(-0.0139960769924853,0.195218999146749,
0.565884339345609));
#36748=CARTESIAN_POINT('Ctrl Pts',(0.0505021771366483,0.199843152198542,
0.562180617662761));
#36749=CARTESIAN_POINT('Ctrl Pts',(0.117518625315826,0.169343225669258,
0.558476895979913));
#36750=CARTESIAN_POINT('Ctrl Pts',(0.156396070392606,0.117671648942254,
0.554773174297065));
#36751=CARTESIAN_POINT('Ctrl Pts',(0.195273515469386,0.0660000722152496,
0.551069452614217));
#36752=CARTESIAN_POINT('Ctrl Pts',(0.206011957443768,-0.00684315470947738,
0.547365730931369));
#36753=CARTESIAN_POINT('Ctrl Pts',(0.183699012241942,-0.0675353292756691,
0.543662009248521));
#36754=CARTESIAN_POINT('Ctrl Pts',(0.161386067040115,-0.128227503841861,
0.539958287565673));
#36755=CARTESIAN_POINT('Ctrl Pts',(0.106021734662079,-0.176768626049519,
0.536254565882826));
#36756=CARTESIAN_POINT('Ctrl Pts',(0.0429328609649713,-0.190953180775813,
0.532550844199978));
#36757=CARTESIAN_POINT('Ctrl Pts',(-0.0201560127321352,-0.205137735502108,
0.52884712251713));
#36758=CARTESIAN_POINT('Ctrl Pts',(-0.0909694277483132,-0.184965722747041,
0.525143400834282));
#36759=CARTESIAN_POINT('Ctrl Pts',(-0.137113234823603,-0.139664987148696,
0.521439679151434));
#36760=CARTESIAN_POINT('Ctrl Pts',(-0.173877852911313,-0.103572077852157,
0.51848877583843));
#36761=CARTESIAN_POINT('Ctrl Pts',(-0.194982335358017,-0.0515275892214865,
0.515537872525427));
#36762=CARTESIAN_POINT('Ctrl Pts',(-0.195458266482996,0.000173443779922018,
0.512586969212423));
#36763=CARTESIAN_POINT('Ctrl Pts',(-0.195491180920002,0.000168629508682236,
0.502413030787576));
#36764=CARTESIAN_POINT('Ctrl Pts',(-0.195010205227512,-0.0526295513449078,
0.505427864266167));
#36765=CARTESIAN_POINT('Ctrl Pts',(-0.172879182329996,-0.105782955367232,
0.508442697744757));
#36766=CARTESIAN_POINT('Ctrl Pts',(-0.134689356786549,-0.142005289462677,
0.511457531223348));
#36767=CARTESIAN_POINT('Ctrl Pts',(-0.0877416010060499,-0.186534356320495,
0.51516374521772));
#36768=CARTESIAN_POINT('Ctrl Pts',(-0.0165250908911267,-0.205476460953673,
0.518869959212092));
#36769=CARTESIAN_POINT('Ctrl Pts',(0.0463414671012952,-0.190155708549211,
0.522576173206464));
#36770=CARTESIAN_POINT('Ctrl Pts',(0.109208025093718,-0.174834956144749,
0.526282387200837));
#36771=CARTESIAN_POINT('Ctrl Pts',(0.163724630963639,-0.125251346702646,
0.529988601195209));
#36772=CARTESIAN_POINT('Ctrl Pts',(0.184921496651671,-0.0641152489120857,
0.533694815189581));
#36773=CARTESIAN_POINT('Ctrl Pts',(0.206118362339704,-0.00297915112152539,
0.537401029183953));
#36774=CARTESIAN_POINT('Ctrl Pts',(0.193995487845847,0.0697094350174917,
0.541107243178325));
#36775=CARTESIAN_POINT('Ctrl Pts',(0.154105412656959,0.120657560296821,
0.544813457172697));
#36776=CARTESIAN_POINT('Ctrl Pts',(0.114215337468071,0.171605685576151,
0.548519671167069));
#36777=CARTESIAN_POINT('Ctrl Pts',(0.0465580615841514,0.200813349995792,
0.552225885161441));
#36778=CARTESIAN_POINT('Ctrl Pts',(-0.0178779150223708,0.194902809680635,
0.555932099155813));
#36779=CARTESIAN_POINT('Ctrl Pts',(-0.0823138916288934,0.188992269365477,
0.559638313150186));
#36780=CARTESIAN_POINT('Ctrl Pts',(-0.143528568958019,0.14796352431552,
0.563344527144558));
#36781=CARTESIAN_POINT('Ctrl Pts',(-0.173484296927877,0.0906086297567353,
0.56705074113893));
#36782=CARTESIAN_POINT('Ctrl Pts',(-0.187931321146693,0.0629475576708828,
0.568838171021812));
#36783=CARTESIAN_POINT('Ctrl Pts',(-0.195107725773013,0.031489133949035,
0.570625600904694));
#36784=CARTESIAN_POINT('Ctrl Pts',(-0.195080468396925,1.8981806121043E-5,
0.572413030787576));
#36785=CARTESIAN_POINT('Origin',(0.,0.,0.));
#36786=CARTESIAN_POINT('',(-0.195470932084261,-0.000171584046685047,0.652586969212424));
#36787=CARTESIAN_POINT('',(-0.195421427783755,-0.000177812761388513,0.642413030787576));
#36788=CARTESIAN_POINT('',(-0.1954,-2.39295984553393E-17,0.));
#36789=CARTESIAN_POINT('Ctrl Pts',(-0.195470932084261,-0.000171584046685047,
0.652586969212424));
#36790=CARTESIAN_POINT('Ctrl Pts',(-0.194992946923152,0.0519398730151351,
0.649612144370087));
#36791=CARTESIAN_POINT('Ctrl Pts',(-0.173506994162404,0.104399306729571,
0.64663731952775));
#36792=CARTESIAN_POINT('Ctrl Pts',(-0.136210733975536,0.140545308526766,
0.643662494685414));
#36793=CARTESIAN_POINT('Ctrl Pts',(-0.0897760782010601,0.185547867567989,
0.639958773002566));
#36794=CARTESIAN_POINT('Ctrl Pts',(-0.0188341937200331,0.205263315093338,
0.636255051319719));
#36795=CARTESIAN_POINT('Ctrl Pts',(0.0441620008484366,0.190672665791667,
0.632551329636871));
#36796=CARTESIAN_POINT('Ctrl Pts',(0.107158195416906,0.176082016489995,
0.628847607954023));
#36797=CARTESIAN_POINT('Ctrl Pts',(0.162208700072817,0.127185270361303,
0.625143886271175));
#36798=CARTESIAN_POINT('Ctrl Pts',(0.184130231899333,0.0663506254660481,
0.621440164588327));
#36799=CARTESIAN_POINT('Ctrl Pts',(0.20605176372585,0.00551598057079281,
0.617736442905479));
#36800=CARTESIAN_POINT('Ctrl Pts',(0.194844322722972,-0.0672565630910262,
0.614032721222632));
#36801=CARTESIAN_POINT('Ctrl Pts',(0.155634840229719,-0.118676637573315,
0.610328999539784));
#36802=CARTESIAN_POINT('Ctrl Pts',(0.116425357736466,-0.170096712055603,
0.606625277856936));
#36803=CARTESIAN_POINT('Ctrl Pts',(0.0492138337528384,-0.200164317358361,
0.602921556174087));
#36804=CARTESIAN_POINT('Ctrl Pts',(-0.0152532956197894,-0.195124792816734,
0.59921783449124));
#36805=CARTESIAN_POINT('Ctrl Pts',(-0.0797204249924167,-0.190085268275106,
0.595514112808392));
#36806=CARTESIAN_POINT('Ctrl Pts',(-0.141443159754043,-0.149938613889095,
0.591810391125544));
#36807=CARTESIAN_POINT('Ctrl Pts',(-0.172185953262212,-0.0930502299740384,
0.588106669442696));
#36808=CARTESIAN_POINT('Ctrl Pts',(-0.187458069522289,-0.0647897528391999,
0.586266769365939));
#36809=CARTESIAN_POINT('Ctrl Pts',(-0.195084923717034,-0.0323977343102287,
0.584426869289181));
#36810=CARTESIAN_POINT('Ctrl Pts',(-0.195079815420139,-3.45302974047446E-6,
0.582586969212423));
#36811=CARTESIAN_POINT('Ctrl Pts',(-0.195080468396925,1.8981806121043E-5,
0.572413030787576));
#36812=CARTESIAN_POINT('Ctrl Pts',(-0.195051207937167,-0.0337638415069996,
0.574331814899066));
#36813=CARTESIAN_POINT('Ctrl Pts',(-0.186720620393942,-0.0675601803708791,
0.576250599010555));
#36814=CARTESIAN_POINT('Ctrl Pts',(-0.170171536425399,-0.0966869859783203,
0.578169383122045));
#36815=CARTESIAN_POINT('Ctrl Pts',(-0.138206269342473,-0.15294666308698,
0.581875597116418));
#36816=CARTESIAN_POINT('Ctrl Pts',(-0.0755789565660301,-0.191784973236686,
0.585581811110791));
#36817=CARTESIAN_POINT('Ctrl Pts',(-0.0109742658556152,-0.195413127900566,
0.589288025105163));
#36818=CARTESIAN_POINT('Ctrl Pts',(0.0536304248547996,-0.199041282564447,
0.592994239099535));
#36819=CARTESIAN_POINT('Ctrl Pts',(0.120212493499187,-0.1674592817425,0.596700453093906));
#36820=CARTESIAN_POINT('Ctrl Pts',(0.158275908344154,-0.115132366886058,
0.600406667088278));
#36821=CARTESIAN_POINT('Ctrl Pts',(0.19633932318912,-0.0628054520296152,
0.60411288108265));
#36822=CARTESIAN_POINT('Ctrl Pts',(0.205884084234667,0.0102663768613233,
0.607819095077022));
#36823=CARTESIAN_POINT('Ctrl Pts',(0.182538483877546,0.0706146370849535,
0.611525309071394));
#36824=CARTESIAN_POINT('Ctrl Pts',(0.159192883520425,0.130962897308584,
0.615231523065767));
#36825=CARTESIAN_POINT('Ctrl Pts',(0.102956921760636,0.178587588864905,
0.618937737060139));
#36826=CARTESIAN_POINT('Ctrl Pts',(0.0395878889512919,0.191675569949154,
0.622643951054511));
#36827=CARTESIAN_POINT('Ctrl Pts',(-0.0237811438580523,0.204763551033402,
0.626350165048883));
#36828=CARTESIAN_POINT('Ctrl Pts',(-0.0942832477169518,0.183314821645578,
0.630056379043255));
#36829=CARTESIAN_POINT('Ctrl Pts',(-0.139626929730598,0.137153365109863,
0.633762593037627));
#36830=CARTESIAN_POINT('Ctrl Pts',(-0.17490486198241,0.101239194403086,
0.63664607228761));
#36831=CARTESIAN_POINT('Ctrl Pts',(-0.194954331224527,0.0503663409317413,
0.639529551537593));
#36832=CARTESIAN_POINT('Ctrl Pts',(-0.195421427783755,-0.000177812761388513,
0.642413030787576));
#36833=CARTESIAN_POINT('Origin',(0.,0.,0.));
#36834=CARTESIAN_POINT('',(-0.195636369417486,0.000113518110994186,0.722586969212423));
#36835=CARTESIAN_POINT('',(-0.195675615924934,8.51174274233985E-5,0.712413030787576));
#36836=CARTESIAN_POINT('',(-0.1954,-2.39295984553393E-17,0.));
#36837=CARTESIAN_POINT('Ctrl Pts',(-0.195636369417486,0.000113518110994186,
0.722586969212423));
#36838=CARTESIAN_POINT('Ctrl Pts',(-0.195682546989371,0.00679235189129894,
0.722204862816689));
#36839=CARTESIAN_POINT('Ctrl Pts',(-0.195370156992351,0.0134668159558925,
0.721822756420955));
#36840=CARTESIAN_POINT('Ctrl Pts',(-0.194684940168549,0.0201027826582277,
0.72144065002522));
#36841=CARTESIAN_POINT('Ctrl Pts',(-0.188043197355288,0.0844245894546327,
0.717736928342373));
#36842=CARTESIAN_POINT('Ctrl Pts',(-0.146373463610807,0.145129475044757,
0.714033206659525));
#36843=CARTESIAN_POINT('Ctrl Pts',(-0.0887378837876281,0.174447515831938,
0.710329484976677));
#36844=CARTESIAN_POINT('Ctrl Pts',(-0.031102303964449,0.203765556619118,
0.706625763293829));
#36845=CARTESIAN_POINT('Ctrl Pts',(0.0424991219374283,0.201696752603353,
0.702922041610981));
#36846=CARTESIAN_POINT('Ctrl Pts',(0.0983968473233738,0.169187494324663,
0.699218319928133));
#36847=CARTESIAN_POINT('Ctrl Pts',(0.154294572709319,0.136678236045973,
0.695514598245285));
#36848=CARTESIAN_POINT('Ctrl Pts',(0.192488597579333,0.0737285235043576,
0.691810876562437));
#36849=CARTESIAN_POINT('Ctrl Pts',(0.195506767226643,0.00913519390189264,
0.68810715487959));
#36850=CARTESIAN_POINT('Ctrl Pts',(0.198524936873952,-0.0554581357005719,
0.684403433196742));
#36851=CARTESIAN_POINT('Ctrl Pts',(0.166367251298559,-0.121695082363886,
0.680699711513894));
#36852=CARTESIAN_POINT('Ctrl Pts',(0.113744494695038,-0.159275037986524,
0.676995989831046));
#36853=CARTESIAN_POINT('Ctrl Pts',(0.0611217380915185,-0.196854993609162,
0.673292268148198));
#36854=CARTESIAN_POINT('Ctrl Pts',(-0.0119660895401274,-0.205777958191125,
0.669588546465349));
#36855=CARTESIAN_POINT('Ctrl Pts',(-0.072084391141631,-0.181962051958034,
0.665884824782502));
#36856=CARTESIAN_POINT('Ctrl Pts',(-0.132202692743136,-0.158146145724943,
0.662181103099654));
#36857=CARTESIAN_POINT('Ctrl Pts',(-0.179351468314497,-0.101591368676797,
0.658477381416807));
#36858=CARTESIAN_POINT('Ctrl Pts',(-0.191962142566216,-0.0381691448741754,
0.654773659733959));
#36859=CARTESIAN_POINT('Ctrl Pts',(-0.19444393828574,-0.0256875756563692,
0.654044762893447));
#36860=CARTESIAN_POINT('Ctrl Pts',(-0.195588048853217,-0.0129400253566584,
0.653315866052935));
#36861=CARTESIAN_POINT('Ctrl Pts',(-0.195470932084261,-0.000171584046685047,
0.652586969212424));
#36862=CARTESIAN_POINT('Ctrl Pts',(-0.195421427783755,-0.000177812761388513,
0.642413030787576));
#36863=CARTESIAN_POINT('Ctrl Pts',(-0.195554703085897,-0.0145994290672205,
0.643235765531965));
#36864=CARTESIAN_POINT('Ctrl Pts',(-0.194093747105224,-0.0289942854151266,
0.644058500276354));
#36865=CARTESIAN_POINT('Ctrl Pts',(-0.190937423221194,-0.0430072724152966,
0.644881235020743));
#36866=CARTESIAN_POINT('Ctrl Pts',(-0.17671897452975,-0.106132269721135,
0.648587449015115));
#36867=CARTESIAN_POINT('Ctrl Pts',(-0.128096816978468,-0.161508080649208,
0.652293663009487));
#36868=CARTESIAN_POINT('Ctrl Pts',(-0.067340953434779,-0.183771382585667,
0.65599987700386));
#36869=CARTESIAN_POINT('Ctrl Pts',(-0.00658508989108841,-0.206034684522128,
0.659706090998232));
#36870=CARTESIAN_POINT('Ctrl Pts',(0.06630447964501,-0.195185477466974,
0.663412304992604));
#36871=CARTESIAN_POINT('Ctrl Pts',(0.117942751209788,-0.156192933591821,
0.667118518986976));
#36872=CARTESIAN_POINT('Ctrl Pts',(0.169581022774564,-0.117200389716668,
0.670824732981348));
#36873=CARTESIAN_POINT('Ctrl Pts',(0.19996799636802,-0.0500645090215166,
0.67453094697572));
#36874=CARTESIAN_POINT('Ctrl Pts',(0.195185778931935,0.0144650188277344,
0.678237160970092));
#36875=CARTESIAN_POINT('Ctrl Pts',(0.190403561495849,0.0789945466769872,
0.681943374964464));
#36876=CARTESIAN_POINT('Ctrl Pts',(0.15045215303022,0.14091772168034,0.685649588958836));
#36877=CARTESIAN_POINT('Ctrl Pts',(0.0936301652358751,0.171872386452436,
0.689355802953208));
#36878=CARTESIAN_POINT('Ctrl Pts',(0.0368081774415317,0.202827051224532,
0.69306201694758));
#36879=CARTESIAN_POINT('Ctrl Pts',(-0.0368843896815252,0.202813205765373,
0.696768230941953));
#36880=CARTESIAN_POINT('Ctrl Pts',(-0.0936947418561655,0.171837191595589,
0.700474444936325));
#36881=CARTESIAN_POINT('Ctrl Pts',(-0.150505094030807,0.140861177425805,
0.704180658930697));
#36882=CARTESIAN_POINT('Ctrl Pts',(-0.190433231257031,0.078922994545395,
0.707886872925069));
#36883=CARTESIAN_POINT('Ctrl Pts',(-0.195191200566454,0.0143916742729559,
0.711593086919441));
#36884=CARTESIAN_POINT('Ctrl Pts',(-0.195542076848464,0.00963281429343837,
0.711866401542153));
#36885=CARTESIAN_POINT('Ctrl Pts',(-0.195701686505733,0.00485985200318871,
0.712139716164864));
#36886=CARTESIAN_POINT('Ctrl Pts',(-0.195675615924934,8.51174274233985E-5,
0.712413030787576));
#36887=CARTESIAN_POINT('Origin',(0.,0.,0.));
#36888=CARTESIAN_POINT('',(-0.195128545551857,9.80157954364874E-5,0.792586969212424));
#36889=CARTESIAN_POINT('',(-0.195166123101285,0.000126544742759004,0.782413030787576));
#36890=CARTESIAN_POINT('',(-0.1954,-2.39295984553393E-17,0.));
#36891=CARTESIAN_POINT('Ctrl Pts',(-0.195128545551857,9.80157954364874E-5,
0.792586969212424));
#36892=CARTESIAN_POINT('Ctrl Pts',(-0.195247914943593,0.0263701155015296,
0.791093859580443));
#36893=CARTESIAN_POINT('Ctrl Pts',(-0.190313505751618,0.0525992349613935,
0.789600749948463));
#36894=CARTESIAN_POINT('Ctrl Pts',(-0.180112460177197,0.0765888339627252,
0.788107640316483));
#36895=CARTESIAN_POINT('Ctrl Pts',(-0.154808334564134,0.136096050365993,
0.784403918633635));
#36896=CARTESIAN_POINT('Ctrl Pts',(-0.0970981193167941,0.181823294990903,
0.780700196950786));
#36897=CARTESIAN_POINT('Ctrl Pts',(-0.0333818027149729,0.192852282969788,
0.776996475267938));
#36898=CARTESIAN_POINT('Ctrl Pts',(0.0303345138868501,0.203881270948674,
0.773292753585091));
#36899=CARTESIAN_POINT('Ctrl Pts',(0.100056931843154,0.180212002281536,
0.769589031902244));
#36900=CARTESIAN_POINT('Ctrl Pts',(0.143890387011628,0.132672168613705,
0.765885310219396));
#36901=CARTESIAN_POINT('Ctrl Pts',(0.187723842180101,0.0851323349458752,
0.762181588536548));
#36902=CARTESIAN_POINT('Ctrl Pts',(0.205668334560742,0.013721936277351,
0.758477866853699));
#36903=CARTESIAN_POINT('Ctrl Pts',(0.18951501609247,-0.0488917833023672,
0.754774145170851));
#36904=CARTESIAN_POINT('Ctrl Pts',(0.173361697624198,-0.111505502882086,
0.751070423488003));
#36905=CARTESIAN_POINT('Ctrl Pts',(0.123110568307013,-0.165322543373001,
0.747366701805156));
#36906=CARTESIAN_POINT('Ctrl Pts',(0.061749399359133,-0.185723879665063,
0.743662980122308));
#36907=CARTESIAN_POINT('Ctrl Pts',(0.000388230411252383,-0.206125215957126,
0.73995925843946));
#36908=CARTESIAN_POINT('Ctrl Pts',(-0.072082978167322,-0.193110848050335,
0.736255536756612));
#36909=CARTESIAN_POINT('Ctrl Pts',(-0.122511706515588,-0.152634300095596,
0.732551815073764));
#36910=CARTESIAN_POINT('Ctrl Pts',(-0.16773779241913,-0.116333645789233,
0.72923019978665));
#36911=CARTESIAN_POINT('Ctrl Pts',(-0.195234952088687,-0.0579449614967985,
0.725908584499537));
#36912=CARTESIAN_POINT('Ctrl Pts',(-0.195636369417486,0.000113518110994186,
0.722586969212423));
#36913=CARTESIAN_POINT('Ctrl Pts',(-0.195675615924934,8.51174274233985E-5,
0.712413030787576));
#36914=CARTESIAN_POINT('Ctrl Pts',(-0.195348162971424,-0.0598867317271105,
0.715845930159236));
#36915=CARTESIAN_POINT('Ctrl Pts',(-0.165727828481393,-0.120138176331325,
0.719278829530897));
#36916=CARTESIAN_POINT('Ctrl Pts',(-0.117884051406102,-0.156237241050387,
0.722711728902558));
#36917=CARTESIAN_POINT('Ctrl Pts',(-0.0662311315437018,-0.195210378436822,
0.72641794289693));
#36918=CARTESIAN_POINT('Ctrl Pts',(0.00666250957372189,-0.206032195545224,
0.730124156891302));
#36919=CARTESIAN_POINT('Ctrl Pts',(0.0674100031098693,-0.183746065393738,
0.733830370885674));
#36920=CARTESIAN_POINT('Ctrl Pts',(0.128157496646017,-0.161459935242253,
0.737536584880046));
#36921=CARTESIAN_POINT('Ctrl Pts',(0.176758842600887,-0.10606585783088,
0.741242798874417));
#36922=CARTESIAN_POINT('Ctrl Pts',(0.19095357026966,-0.0429355222190436,
0.744949012868789));
#36923=CARTESIAN_POINT('Ctrl Pts',(0.205148297938434,0.0201948133927931,
0.748655226863161));
#36924=CARTESIAN_POINT('Ctrl Pts',(0.184936407321109,0.0910614072050953,
0.752361440857534));
#36925=CARTESIAN_POINT('Ctrl Pts',(0.139575382755531,0.137205822017881,
0.756067654851907));
#36926=CARTESIAN_POINT('Ctrl Pts',(0.0942143581899539,0.183350236830666,
0.759773868846279));
#36927=CARTESIAN_POINT('Ctrl Pts',(0.0237041996761252,0.204772472643938,
0.76348008284065));
#36928=CARTESIAN_POINT('Ctrl Pts',(-0.0396599106844383,0.191660680765389,
0.767186296835022));
#36929=CARTESIAN_POINT('Ctrl Pts',(-0.103024021045003,0.178548888886839,
0.770892510829394));
#36930=CARTESIAN_POINT('Ctrl Pts',(-0.159242083252301,0.130903069316467,
0.774598724823766));
#36931=CARTESIAN_POINT('Ctrl Pts',(-0.182565005336597,0.0705460409477194,
0.778304938818139));
#36932=CARTESIAN_POINT('Ctrl Pts',(-0.19118230851659,0.0482454556858425,
0.779674302807951));
#36933=CARTESIAN_POINT('Ctrl Pts',(-0.195308968355645,0.0242096139413284,
0.781043666797764));
#36934=CARTESIAN_POINT('Ctrl Pts',(-0.195166123101285,0.000126544742759004,
0.782413030787576));
#36935=CARTESIAN_POINT('Origin',(0.,0.,0.));
#36936=CARTESIAN_POINT('',(-0.195279013340439,-0.000168009551267251,0.862586969212423));
#36937=CARTESIAN_POINT('',(-0.195215444869335,-0.000150235120299324,0.852413030787576));
#36938=CARTESIAN_POINT('',(-0.1954,-2.39295984553393E-17,0.));
#36939=CARTESIAN_POINT('Ctrl Pts',(-0.195279013340439,-0.000168009551267251,
0.862586969212423));
#36940=CARTESIAN_POINT('Ctrl Pts',(-0.194903607268958,0.0455640131522026,
0.859982856344197));
#36941=CARTESIAN_POINT('Ctrl Pts',(-0.178871895344458,0.0915331173731693,
0.857378743475971));
#36942=CARTESIAN_POINT('Ctrl Pts',(-0.149539281844263,0.126270942713959,
0.854774630607745));
#36943=CARTESIAN_POINT('Ctrl Pts',(-0.107820722729247,0.175677110357261,
0.851070908924897));
#36944=CARTESIAN_POINT('Ctrl Pts',(-0.0391968436807465,0.202364430724413,
0.847367187242049));
#36945=CARTESIAN_POINT('Ctrl Pts',(0.024939826400162,0.194124580780539,
0.843663465559201));
#36946=CARTESIAN_POINT('Ctrl Pts',(0.0890764964810705,0.185884730836666,
0.839959743876352));
#36947=CARTESIAN_POINT('Ctrl Pts',(0.148725957594388,0.142717710581768,
0.836256022193505));
#36948=CARTESIAN_POINT('Ctrl Pts',(0.176601098282085,0.0843706103134459,
0.832552300510657));
#36949=CARTESIAN_POINT('Ctrl Pts',(0.204476238969783,0.0260235100451228,
0.828848578827809));
#36950=CARTESIAN_POINT('Ctrl Pts',(0.200577059231861,-0.0475036702366233,
0.825144857144961));
#36951=CARTESIAN_POINT('Ctrl Pts',(0.166687269277466,-0.102575348200379,
0.821441135462114));
#36952=CARTESIAN_POINT('Ctrl Pts',(0.132797479323072,-0.157647026164133,
0.817737413779266));
#36953=CARTESIAN_POINT('Ctrl Pts',(0.0689170791522051,-0.194263201809897,
0.814033692096418));
#36954=CARTESIAN_POINT('Ctrl Pts',(0.00426865627857745,-0.195673519857469,
0.81032997041357));
#36955=CARTESIAN_POINT('Ctrl Pts',(-0.060379766595052,-0.197083837905041,
0.806626248730722));
#36956=CARTESIAN_POINT('Ctrl Pts',(-0.125796212171444,-0.16328829835442,
0.802922527047874));
#36957=CARTESIAN_POINT('Ctrl Pts',(-0.162055416970245,-0.109746934488294,
0.799218805365026));
#36958=CARTESIAN_POINT('Ctrl Pts',(-0.183697171385623,-0.0777901098892797,
0.797008193314158));
#36959=CARTESIAN_POINT('Ctrl Pts',(-0.194951814111497,-0.0387989405753114,
0.794797581263291));
#36960=CARTESIAN_POINT('Ctrl Pts',(-0.195128545551857,9.80157954364874E-5,
0.792586969212424));
#36961=CARTESIAN_POINT('Ctrl Pts',(-0.195166123101285,0.000126544742759004,
0.782413030787576));
#36962=CARTESIAN_POINT('Ctrl Pts',(-0.194922354508138,-0.0409717467160323,
0.784749880792136));
#36963=CARTESIAN_POINT('Ctrl Pts',(-0.182244856716882,-0.0822075748123473,
0.787086730796695));
#36964=CARTESIAN_POINT('Ctrl Pts',(-0.158232634722073,-0.115191832939155,
0.789423580801255));
#36965=CARTESIAN_POINT('Ctrl Pts',(-0.120149560061961,-0.167504441290151,
0.793129794795627));
#36966=CARTESIAN_POINT('Ctrl Pts',(-0.0535556287804454,-0.199061420825021,
0.796836008789999));
#36967=CARTESIAN_POINT('Ctrl Pts',(0.0110476940437387,-0.195408990384897,
0.800542222784371));
#36968=CARTESIAN_POINT('Ctrl Pts',(0.0756510168679237,-0.191756559944773,
0.804248436778743));
#36969=CARTESIAN_POINT('Ctrl Pts',(0.138263731234777,-0.152894719529654,
0.807954650773115));
#36970=CARTESIAN_POINT('Ctrl Pts',(0.170207855773424,-0.0966230350379699,
0.811660864767488));
#36971=CARTESIAN_POINT('Ctrl Pts',(0.202151980312072,-0.0403513505462853,
0.81536707876186));
#36972=CARTESIAN_POINT('Ctrl Pts',(0.203427515022513,0.0333301780219651,
0.819073292756232));
#36973=CARTESIAN_POINT('Ctrl Pts',(0.173450237337761,0.0906738122863988,
0.822779506750604));
#36974=CARTESIAN_POINT('Ctrl Pts',(0.143472959653009,0.148017446550833,
0.826485720744976));
#36975=CARTESIAN_POINT('Ctrl Pts',(0.0822428695730641,0.189023186511451,
0.830191934739348));
#36976=CARTESIAN_POINT('Ctrl Pts',(0.0178046765554912,0.194909513773745,
0.83389814873372));
#36977=CARTESIAN_POINT('Ctrl Pts',(-0.0466335164620799,0.200795841036038,
0.837604362728092));
#36978=CARTESIAN_POINT('Ctrl Pts',(-0.114279812417278,0.171562755600011,
0.841310576722464));
#36979=CARTESIAN_POINT('Ctrl Pts',(-0.154150740386038,0.120599644714809,
0.845016790716836));
#36980=CARTESIAN_POINT('Ctrl Pts',(-0.180673309918174,0.0866984359672774,
0.84748220407375));
#36981=CARTESIAN_POINT('Ctrl Pts',(-0.194905131081074,0.0431815751432988,
0.849947617430663));
#36982=CARTESIAN_POINT('Ctrl Pts',(-0.195215444869335,-0.000150235120299324,
0.852413030787576));
#36983=CARTESIAN_POINT('Origin',(0.,0.,0.));
#36984=CARTESIAN_POINT('',(-0.195719986784682,3.71606954582295E-6,0.932586969212424));
#36985=CARTESIAN_POINT('',(-0.195707453392556,-4.66568259871601E-5,0.922413030787576));
#36986=CARTESIAN_POINT('',(-0.1954,-2.39295984553393E-17,0.));
#36987=CARTESIAN_POINT('Ctrl Pts',(-0.195719986784682,3.71606954582295E-6,
0.932586969212424));
#36988=CARTESIAN_POINT('Ctrl Pts',(-0.195738156138108,0.0648665395087412,
0.928871853107952));
#36989=CARTESIAN_POINT('Ctrl Pts',(-0.160275715576186,0.129712057687137,
0.925156737003479));
#36990=CARTESIAN_POINT('Ctrl Pts',(-0.10568144211536,0.164735485073218,
0.921441620899007));
#36991=CARTESIAN_POINT('Ctrl Pts',(-0.0512546116502832,0.199651494094127,
0.917737899216159));
#36992=CARTESIAN_POINT('Ctrl Pts',(0.0221865722997436,0.204928064005996,
0.914034177533311));
#36993=CARTESIAN_POINT('Ctrl Pts',(0.0810458692323854,0.178151382429043,
0.910330455850463));
#36994=CARTESIAN_POINT('Ctrl Pts',(0.139905166165026,0.151374700852089,
0.906626734167615));
#36995=CARTESIAN_POINT('Ctrl Pts',(0.184182576080283,0.0925447677863139,
0.902923012484767));
#36996=CARTESIAN_POINT('Ctrl Pts',(0.193623051178265,0.0285737974246437,
0.899219290801919));
#36997=CARTESIAN_POINT('Ctrl Pts',(0.203063526276248,-0.0353971729370283,
0.895515569119071));
#36998=CARTESIAN_POINT('Ctrl Pts',(0.177667066556955,-0.104509180594595,
0.891811847436224));
#36999=CARTESIAN_POINT('Ctrl Pts',(0.129051481285208,-0.147146399547075,
0.888108125753376));
#37000=CARTESIAN_POINT('Ctrl Pts',(0.0804358960134615,-0.189783618499555,
0.884404404070528));
#37001=CARTESIAN_POINT('Ctrl Pts',(0.00860118518926115,-0.205946048746948,
0.88070068238768));
#37002=CARTESIAN_POINT('Ctrl Pts',(-0.0535913025040727,-0.188240059832962,
0.876996960704832));
#37003=CARTESIAN_POINT('Ctrl Pts',(-0.115783790197406,-0.170534070918976,
0.873293239021984));
#37004=CARTESIAN_POINT('Ctrl Pts',(-0.168334054759872,-0.118959662843613,
0.869589517339136));
#37005=CARTESIAN_POINT('Ctrl Pts',(-0.187202567450341,-0.0571099513462054,
0.865885795656288));
#37006=CARTESIAN_POINT('Ctrl Pts',(-0.192804495632289,-0.0387472087407564,
0.864786186841667));
#37007=CARTESIAN_POINT('Ctrl Pts',(-0.195437531748109,-0.0194787452297348,
0.863686578027045));
#37008=CARTESIAN_POINT('Ctrl Pts',(-0.195279013340439,-0.000168009551267251,
0.862586969212423));
#37009=CARTESIAN_POINT('Ctrl Pts',(-0.195215444869335,-0.000150235120299324,
0.852413030787576));
#37010=CARTESIAN_POINT('Ctrl Pts',(-0.195371620524508,-0.021958398707372,
0.853653831425035));
#37011=CARTESIAN_POINT('Ctrl Pts',(-0.192001564940553,-0.0437196901383431,
0.854894632062494));
#37012=CARTESIAN_POINT('Ctrl Pts',(-0.184897391479539,-0.0641847309864828,
0.856135432699953));
#37013=CARTESIAN_POINT('Ctrl Pts',(-0.163677554621959,-0.125312859468192,
0.859841646694325));
#37014=CARTESIAN_POINT('Ctrl Pts',(-0.10914232092448,-0.174875980097234,
0.863547860688697));
#37015=CARTESIAN_POINT('Ctrl Pts',(-0.0462700104058479,-0.190173108515756,
0.867254074683069));
#37016=CARTESIAN_POINT('Ctrl Pts',(0.0166023001127845,-0.205470236934278,
0.870960288677441));
#37017=CARTESIAN_POINT('Ctrl Pts',(0.0878116874525705,-0.186501373142281,
0.874666502671813));
#37018=CARTESIAN_POINT('Ctrl Pts',(0.134742707561642,-0.141954668207959,
0.878372716666185));
#37019=CARTESIAN_POINT('Ctrl Pts',(0.181673727670714,-0.0974079632736377,
0.882078930660557));
#37020=CARTESIAN_POINT('Ctrl Pts',(0.204326380549072,-0.0272834171969915,
0.885785144654929));
#37021=CARTESIAN_POINT('Ctrl Pts',(0.192325259761237,0.0363004067433246,
0.889491358649301));
#37022=CARTESIAN_POINT('Ctrl Pts',(0.180324138973402,0.0998842306836407,
0.893197572643673));
#37023=CARTESIAN_POINT('Ctrl Pts',(0.133669244519374,0.156927332487627,
0.896903786638045));
#37024=CARTESIAN_POINT('Ctrl Pts',(0.0737295301650971,0.181302734225987,
0.900610000632418));
#37025=CARTESIAN_POINT('Ctrl Pts',(0.0137898158108199,0.205678135964346,
0.90431621462679));
#37026=CARTESIAN_POINT('Ctrl Pts',(-0.059434718443707,0.19738583763708,
0.908022428621162));
#37027=CARTESIAN_POINT('Ctrl Pts',(-0.112405647662483,0.160223891616111,
0.911728642615534));
#37028=CARTESIAN_POINT('Ctrl Pts',(-0.163307724594775,0.124513356361944,
0.915290105339548));
#37029=CARTESIAN_POINT('Ctrl Pts',(-0.195507366281261,0.0621442230158499,
0.918851568063562));
#37030=CARTESIAN_POINT('Ctrl Pts',(-0.195707453392556,-4.66568259871601E-5,
0.922413030787576));
#37031=CARTESIAN_POINT('Origin',(0.,0.,0.));
#37032=CARTESIAN_POINT('',(-0.195268202714777,0.000165579016441021,1.00258696921242));
#37033=CARTESIAN_POINT('',(-0.19535343393295,0.000178280253715055,0.992413030787576));
#37034=CARTESIAN_POINT('',(-0.1954,-2.39295984553393E-17,0.));
#37035=CARTESIAN_POINT('Ctrl Pts',(-0.195268202714777,0.000165579016441021,
1.00258696921242));
#37036=CARTESIAN_POINT('Ctrl Pts',(-0.19542709496717,0.0198793394721131,
1.00146457155455));
#37037=CARTESIAN_POINT('Ctrl Pts',(-0.192681564478375,0.0395498739780043,
1.00034217389668));
#37038=CARTESIAN_POINT('Ctrl Pts',(-0.186848643290836,0.0582577638715851,
0.999219776238813));
#37039=CARTESIAN_POINT('Ctrl Pts',(-0.167600993827966,0.11999062383733,
0.995516054555966));
#37040=CARTESIAN_POINT('Ctrl Pts',(-0.114735119634562,0.171241362792136,
0.991812332873117));
#37041=CARTESIAN_POINT('Ctrl Pts',(-0.0524351231736321,0.18856531990772,
0.988108611190269));
#37042=CARTESIAN_POINT('Ctrl Pts',(0.00986487328729629,0.205889277023303,
0.984404889507421));
#37043=CARTESIAN_POINT('Ctrl Pts',(0.0815989920157509,0.189286452299667,
0.980701167824573));
#37044=CARTESIAN_POINT('Ctrl Pts',(0.129952003507049,0.146351732792493,
0.976997446141725));
#37045=CARTESIAN_POINT('Ctrl Pts',(0.178305014998348,0.103417013285319,
0.973293724458878));
#37046=CARTESIAN_POINT('Ctrl Pts',(0.20327691925249,0.0341503989946047,
0.969590002776029));
#37047=CARTESIAN_POINT('Ctrl Pts',(0.19344406978275,-0.0297614493697593,
0.965886281093181));
#37048=CARTESIAN_POINT('Ctrl Pts',(0.18361122031301,-0.0936732977341234,
0.962182559410334));
#37049=CARTESIAN_POINT('Ctrl Pts',(0.138973617119388,-0.152230380172138,
0.958478837727486));
#37050=CARTESIAN_POINT('Ctrl Pts',(0.0799511084736072,-0.178645358874384,
0.954775116044638));
#37051=CARTESIAN_POINT('Ctrl Pts',(0.0209285998278261,-0.20506033757663,
0.95107139436179));
#37052=CARTESIAN_POINT('Ctrl Pts',(-0.0524788142701144,-0.199333212543108,
0.947367672678942));
#37053=CARTESIAN_POINT('Ctrl Pts',(-0.106690354347858,-0.16408387214268,
0.943663950996094));
#37054=CARTESIAN_POINT('Ctrl Pts',(-0.160735113766186,-0.128942975594381,
0.93997162373487));
#37055=CARTESIAN_POINT('Ctrl Pts',(-0.195701928883641,-0.0644612332051665,
0.936279296473647));
#37056=CARTESIAN_POINT('Ctrl Pts',(-0.195719986784682,3.71606954582295E-6,
0.932586969212424));
#37057=CARTESIAN_POINT('Ctrl Pts',(-0.195707453392556,-4.66568259871601E-5,
0.922413030787576));
#37058=CARTESIAN_POINT('Ctrl Pts',(-0.195715585687005,-0.00257432861687418,
0.922557782057934));
#37059=CARTESIAN_POINT('Ctrl Pts',(-0.195670857405051,-0.00510170594794435,
0.922702533328292));
#37060=CARTESIAN_POINT('Ctrl Pts',(-0.195572375776859,-0.00762698699047084,
0.92284728459865));
#37061=CARTESIAN_POINT('Ctrl Pts',(-0.193050850489432,-0.0722843258614067,
0.926553498593022));
#37062=CARTESIAN_POINT('Ctrl Pts',(-0.155290475731554,-0.135567409888606,
0.930259712587394));
#37063=CARTESIAN_POINT('Ctrl Pts',(-0.0995863227266852,-0.168491214354887,
0.933965926581766));
#37064=CARTESIAN_POINT('Ctrl Pts',(-0.0438821697218168,-0.201415018821168,
0.937672140576139));
#37065=CARTESIAN_POINT('Ctrl Pts',(0.0297657615300397,-0.203979543726533,
0.94137835457051));
#37066=CARTESIAN_POINT('Ctrl Pts',(0.0876251218790847,-0.175010180082627,
0.945084568564882));
#37067=CARTESIAN_POINT('Ctrl Pts',(0.145484482228131,-0.146040816438721,
0.948790782559255));
#37068=CARTESIAN_POINT('Ctrl Pts',(0.187555271674363,-0.0855375642455424,
0.952496996553627));
#37069=CARTESIAN_POINT('Ctrl Pts',(0.194568154283725,-0.021212227253196,
0.956203210547999));
#37070=CARTESIAN_POINT('Ctrl Pts',(0.201581036893087,0.0431131097391505,
0.959909424542371));
#37071=CARTESIAN_POINT('Ctrl Pts',(0.173536012665579,0.111260531530666,
0.963615638536743));
#37072=CARTESIAN_POINT('Ctrl Pts',(0.123278314419194,0.152017044141902,
0.967321852531115));
#37073=CARTESIAN_POINT('Ctrl Pts',(0.0730206161728088,0.192773556753138,
0.971028066525487));
#37074=CARTESIAN_POINT('Ctrl Pts',(0.000550243907548716,0.206139160184095,
0.974734280519859));
#37075=CARTESIAN_POINT('Ctrl Pts',(-0.0609398062732146,0.185992111567971,
0.978440494514231));
#37076=CARTESIAN_POINT('Ctrl Pts',(-0.122429856453979,0.165845062951848,
0.982146708508603));
#37077=CARTESIAN_POINT('Ctrl Pts',(-0.172939584550245,0.112185362288641,
0.985852922502976));
#37078=CARTESIAN_POINT('Ctrl Pts',(-0.189334427223443,0.0495903289718102,
0.989559136497348));
#37079=CARTESIAN_POINT('Ctrl Pts',(-0.193542598326109,0.0335236538822793,
0.990510434594091));
#37080=CARTESIAN_POINT('Ctrl Pts',(-0.195503184094814,0.0168682937546108,
0.991461732690834));
#37081=CARTESIAN_POINT('Ctrl Pts',(-0.19535343393295,0.000178280253715055,
0.992413030787576));
#37082=CARTESIAN_POINT('Origin',(0.,0.,0.));
#37083=CARTESIAN_POINT('',(-0.195129684289216,-0.000113636086278679,1.07258696921242));
#37084=CARTESIAN_POINT('',(-0.195093054978418,-5.50606481354719E-5,1.06241303078758));
#37085=CARTESIAN_POINT('',(-0.1954,-2.39295984553393E-17,0.));
#37086=CARTESIAN_POINT('Ctrl Pts',(-0.195129684289216,-0.000113636086278679,
1.07258696921242));
#37087=CARTESIAN_POINT('Ctrl Pts',(-0.194942963316978,0.0391854106201406,
1.07035356831831));
#37088=CARTESIAN_POINT('Ctrl Pts',(-0.183442754086643,0.0785903964976412,
1.06812016742419));
#37089=CARTESIAN_POINT('Ctrl Pts',(-0.161381630858742,0.110744756631717,
1.06588676653008));
#37090=CARTESIAN_POINT('Ctrl Pts',(-0.124796949325566,0.164067382739912,
1.06218304484723));
#37091=CARTESIAN_POINT('Ctrl Pts',(-0.0591690439027595,0.197450300329055,
1.05847932316438));
#37092=CARTESIAN_POINT('Ctrl Pts',(0.00547076636758263,0.195640786233593,
1.05477560148153));
#37093=CARTESIAN_POINT('Ctrl Pts',(0.0701105766379276,0.19383127213813,
1.05107187979868));
#37094=CARTESIAN_POINT('Ctrl Pts',(0.133762291755807,0.156829326358058,
1.04736815811584));
#37095=CARTESIAN_POINT('Ctrl Pts',(0.167312833478204,0.101552035674769,
1.04366443643299));
#37096=CARTESIAN_POINT('Ctrl Pts',(0.200863375200599,0.0462747449914819,
1.03996071475014));
#37097=CARTESIAN_POINT('Ctrl Pts',(0.204312743527515,-0.0272778905950186,
1.03625699306729));
#37098=CARTESIAN_POINT('Ctrl Pts',(0.17608042651717,-0.0854535269464722,
1.03255327138444));
#37099=CARTESIAN_POINT('Ctrl Pts',(0.147848109506825,-0.143629163297926,
1.0288495497016));
#37100=CARTESIAN_POINT('Ctrl Pts',(0.0879341071592168,-0.186427800414334,
1.02514582801875));
#37101=CARTESIAN_POINT('Ctrl Pts',(0.0237478981470821,-0.194273555725334,
1.0214421063359));
#37102=CARTESIAN_POINT('Ctrl Pts',(-0.0404383108650536,-0.202119311036335,
1.01773838465305));
#37103=CARTESIAN_POINT('Ctrl Pts',(-0.108896726541717,-0.175012184541928,
1.0140346629702));
#37104=CARTESIAN_POINT('Ctrl Pts',(-0.15031122201388,-0.125351130806383,
1.01033094128736));
#37105=CARTESIAN_POINT('Ctrl Pts',(-0.17917522457641,-0.0907396556226723,
1.00774961726238));
#37106=CARTESIAN_POINT('Ctrl Pts',(-0.194902777514884,-0.0451727225472274,
1.0051682932374));
#37107=CARTESIAN_POINT('Ctrl Pts',(-0.195268202714777,0.000165579016441021,
1.00258696921242));
#37108=CARTESIAN_POINT('Ctrl Pts',(-0.19535343393295,0.000178280253715055,
0.992413030787576));
#37109=CARTESIAN_POINT('Ctrl Pts',(-0.194919764294582,-0.0481552375812319,
0.995167946685205));
#37110=CARTESIAN_POINT('Ctrl Pts',(-0.176787653021499,-0.0967793777264111,
0.997922862582834));
#37111=CARTESIAN_POINT('Ctrl Pts',(-0.144290486192301,-0.132238333502052,
1.00067777848046));
#37112=CARTESIAN_POINT('Ctrl Pts',(-0.100571745237828,-0.179941596688631,
1.00438399247484));
#37113=CARTESIAN_POINT('Ctrl Pts',(-0.0308543060787511,-0.203817757091334,
1.00809020646921));
#37114=CARTESIAN_POINT('Ctrl Pts',(0.0329297761185238,-0.192930969998698,
1.01179642046358));
#37115=CARTESIAN_POINT('Ctrl Pts',(0.0967138583157977,-0.182044182906063,
1.01550263445795));
#37116=CARTESIAN_POINT('Ctrl Pts',(0.15456458355127,-0.136394448318089,
1.01920884845232));
#37117=CARTESIAN_POINT('Ctrl Pts',(0.179984980484802,-0.076890421197536,
1.0229150624467));
#37118=CARTESIAN_POINT('Ctrl Pts',(0.205405377418334,-0.0173863940769825,
1.02662127644107));
#37119=CARTESIAN_POINT('Ctrl Pts',(0.198395446049928,0.05597192557615,1.03032749043544));
#37120=CARTESIAN_POINT('Ctrl Pts',(0.162166047466929,0.109585000349956,
1.03403370442981));
#37121=CARTESIAN_POINT('Ctrl Pts',(0.12593664888393,0.163198075123761,1.03773991842419));
#37122=CARTESIAN_POINT('Ctrl Pts',(0.0604877830863377,0.19706590501824,
1.04144613241856));
#37123=CARTESIAN_POINT('Ctrl Pts',(-0.0042038551539475,0.195675976549601,
1.04515234641293));
#37124=CARTESIAN_POINT('Ctrl Pts',(-0.0688954933942345,0.194286048080962,
1.0488585604073));
#37125=CARTESIAN_POINT('Ctrl Pts',(-0.132829904077215,0.157638361249205,
1.05256477440167));
#37126=CARTESIAN_POINT('Ctrl Pts',(-0.166723158702796,0.102518946943711,
1.05627098839605));
#37127=CARTESIAN_POINT('Ctrl Pts',(-0.185446111291195,0.0720704641366568,
1.05831833585989));
#37128=CARTESIAN_POINT('Ctrl Pts',(-0.195001820365716,0.0359852200961074,
1.06036568332373));
#37129=CARTESIAN_POINT('Ctrl Pts',(-0.195093054978418,-5.50606481354719E-5,
1.06241303078758));
#37130=CARTESIAN_POINT('Origin',(0.,0.,-0.129405622560369));
#37131=CARTESIAN_POINT('',(-0.155334812646815,-9.04610707407963E-5,1.09559437743963));
#37132=CARTESIAN_POINT('',(-0.155659711405804,-0.000105088068675666,1.10940562256037));
#37133=CARTESIAN_POINT('',(-0.15555,-2.01987159101623E-14,-0.129405622560369));
#37134=CARTESIAN_POINT('',(0.0499806597877791,0.147301514408978,1.14445));
#37135=CARTESIAN_POINT('Ctrl Pts',(-0.155334812646815,-9.04610707408108E-5,
1.09559437743963));
#37136=CARTESIAN_POINT('Ctrl Pts',(-0.155432667860164,-0.0206859868644216,
1.09706469822836));
#37137=CARTESIAN_POINT('Ctrl Pts',(-0.142041322258558,-0.0930327919713715,
1.10223874069994));
#37138=CARTESIAN_POINT('Ctrl Pts',(-0.0324962964057439,-0.180887727526569,
1.11111650485437));
#37139=CARTESIAN_POINT('Ctrl Pts',(0.134445241673909,-0.125560970886474,
1.12222766990291));
#37140=CARTESIAN_POINT('Ctrl Pts',(0.178171768593789,0.0450698535437549,
1.13333883495146));
#37141=CARTESIAN_POINT('Ctrl Pts',(0.0989503531151977,0.130685679928735,
1.14074627831715));
#37142=CARTESIAN_POINT('Ctrl Pts',(0.0499806597877626,0.147301514408983,
1.14445));
#37143=CARTESIAN_POINT('',(0.155548765964692,0.000619602180124784,1.14445));
#37144=CARTESIAN_POINT('Origin',(0.,0.,1.14445));
#37145=CARTESIAN_POINT('Ctrl Pts',(-0.155659711405804,-0.00010508806867568,
1.10940562256037));
#37146=CARTESIAN_POINT('Ctrl Pts',(-0.155726922058417,-0.0079449137192624,
1.1099684397238));
#37147=CARTESIAN_POINT('Ctrl Pts',(-0.151630179095532,-0.0673453815214831,
1.1142374708816));
#37148=CARTESIAN_POINT('Ctrl Pts',(-0.075277483453787,-0.167898453189698,
1.12221271603377));
#37149=CARTESIAN_POINT('Ctrl Pts',(0.100462758039806,-0.153944373403644,
1.13333135801688));
#37150=CARTESIAN_POINT('Ctrl Pts',(0.155754888396286,-0.0511266487217653,
1.14074378600563));
#37151=CARTESIAN_POINT('Ctrl Pts',(0.155548765964692,0.000619602180124784,
1.14445));
#37152=CARTESIAN_POINT('Origin',(0.,0.,-0.129405622560369));
#37153=CARTESIAN_POINT('',(-0.155445081536763,0.000131810726739325,1.02559437743963));
#37154=CARTESIAN_POINT('',(-0.155305653540906,-4.38315446397164E-5,1.03940562256037));
#37155=CARTESIAN_POINT('',(-0.15555,-2.01987159101623E-14,-0.129405622560369));
#37156=CARTESIAN_POINT('Ctrl Pts',(-0.155445081536763,0.000131810726739319,
1.02559437743963));
#37157=CARTESIAN_POINT('Ctrl Pts',(-0.155154181384031,-0.0359601688445403,
1.02817570146461));
#37158=CARTESIAN_POINT('Ctrl Pts',(-0.124670140973274,-0.124280598265434,
1.03446074717243));
#37159=CARTESIAN_POINT('Ctrl Pts',(0.0223056668548975,-0.182477852394609,
1.04444951456311));
#37160=CARTESIAN_POINT('Ctrl Pts',(0.165390974917898,-0.0802670846854376,
1.05556067961165));
#37161=CARTESIAN_POINT('Ctrl Pts',(0.157153269033781,0.0953897085409752,
1.06667184466019));
#37162=CARTESIAN_POINT('Ctrl Pts',(0.00514163720288116,0.183756944970195,
1.07778300970874));
#37163=CARTESIAN_POINT('Ctrl Pts',(-0.130849536725084,0.114582374749785,
1.08742385396855));
#37164=CARTESIAN_POINT('Ctrl Pts',(-0.155186171668149,0.0311939131113674,
1.09336097654551));
#37165=CARTESIAN_POINT('Ctrl Pts',(-0.155334812646815,-9.04610707408108E-5,
1.09559437743963));
#37166=CARTESIAN_POINT('Ctrl Pts',(-0.155305653540906,-4.38315446397077E-5,
1.03940562256037));
#37167=CARTESIAN_POINT('Ctrl Pts',(-0.155364500629154,-0.0232901140548306,
1.0410644890909));
#37168=CARTESIAN_POINT('Ctrl Pts',(-0.139557528484751,-0.0983968830408974,
1.0464295696158));
#37169=CARTESIAN_POINT('Ctrl Pts',(-0.0231259578302998,-0.182421227428175,
1.05550086413507));
#37170=CARTESIAN_POINT('Ctrl Pts',(0.140774638007895,-0.11829694620695,
1.06661950611819));
#37171=CARTESIAN_POINT('Ctrl Pts',(0.175706993010233,0.0541796064983141,
1.07773814810131));
#37172=CARTESIAN_POINT('Ctrl Pts',(0.0497080432048737,0.177049779856472,
1.08885679008442));
#37173=CARTESIAN_POINT('Ctrl Pts',(-0.113185991314487,0.139680492671116,
1.09941261490411));
#37174=CARTESIAN_POINT('Ctrl Pts',(-0.155284332390808,0.0436812153822664,
1.10626222572943));
#37175=CARTESIAN_POINT('Ctrl Pts',(-0.155659711405804,-0.00010508806867568,
1.10940562256037));
#37176=CARTESIAN_POINT('Origin',(0.,0.,-0.129405622560369));
#37177=CARTESIAN_POINT('',(-0.155804728476752,2.95821195149996E-6,0.95559437743963));
#37178=CARTESIAN_POINT('',(-0.155512930646214,0.000141921665610299,0.969405622560371));
#37179=CARTESIAN_POINT('',(-0.15555,-2.01987159101623E-14,-0.129405622560369));
#37180=CARTESIAN_POINT('Ctrl Pts',(-0.155804728476752,2.95821195150548E-6,
0.95559437743963));
#37181=CARTESIAN_POINT('Ctrl Pts',(-0.155790353315504,-0.0513149683984934,
0.959286704700854));
#37182=CARTESIAN_POINT('Ctrl Pts',(-0.100033131917675,-0.154135965233235,
0.966682753644926));
#37183=CARTESIAN_POINT('Ctrl Pts',(0.0750970673805211,-0.167799333720618,
0.977782524271844));
#37184=CARTESIAN_POINT('Ctrl Pts',(0.181699613594968,-0.0279545920640164,
0.988893689320389));
#37185=CARTESIAN_POINT('Ctrl Pts',(0.122062258834496,0.137466418983892,
1.00000485436893));
#37186=CARTESIAN_POINT('Ctrl Pts',(-0.0492515922639386,0.177116921324136,
1.01111601941748));
#37187=CARTESIAN_POINT('Ctrl Pts',(-0.146173837715872,0.0831558022400444,
1.01964586044104));
#37188=CARTESIAN_POINT('Ctrl Pts',(-0.155571569202373,0.015825134364817,
1.02447197978176));
#37189=CARTESIAN_POINT('Ctrl Pts',(-0.155445081536763,0.000131810726739319,
1.02559437743963));
#37190=CARTESIAN_POINT('Ctrl Pts',(-0.155512930646214,0.000141921665610296,
0.969405622560371));
#37191=CARTESIAN_POINT('Ctrl Pts',(-0.155167703869094,-0.0383344278698275,
0.972160538458));
#37192=CARTESIAN_POINT('Ctrl Pts',(-0.121314953523015,-0.129115961930375,
0.97862166835));
#37193=CARTESIAN_POINT('Ctrl Pts',(0.0309373610575528,-0.181257875466721,
0.988789012236375));
#37194=CARTESIAN_POINT('Ctrl Pts',(0.169095195914933,-0.0722381792257861,
0.999907654219489));
#37195=CARTESIAN_POINT('Ctrl Pts',(0.152354231364944,0.102954552944809,
1.01102629620261));
#37196=CARTESIAN_POINT('Ctrl Pts',(-0.00394931635484403,0.183836962465064,
1.02214493818572));
#37197=CARTESIAN_POINT('Ctrl Pts',(-0.133855689695156,0.109373648628768,
1.03160471363831));
#37198=CARTESIAN_POINT('Ctrl Pts',(-0.15523302537302,0.0286463714736223,
1.03735827509653));
#37199=CARTESIAN_POINT('Ctrl Pts',(-0.155305653540906,-4.38315446397077E-5,
1.03940562256037));
#37200=CARTESIAN_POINT('Origin',(0.,0.,-0.129405622560369));
#37201=CARTESIAN_POINT('',(-0.155453687436568,-0.000133745576774406,0.885594377439631));
#37202=CARTESIAN_POINT('',(-0.155794751152569,-3.71416033132788E-5,0.899405622560372));
#37203=CARTESIAN_POINT('',(-0.15555,-2.01987159101623E-14,-0.129405622560369));
#37204=CARTESIAN_POINT('Ctrl Pts',(-0.155453687436568,-0.000133745576774402,
0.885594377439631));
#37205=CARTESIAN_POINT('Ctrl Pts',(-0.155579877499581,-0.0155062375664632,
0.886693986254252));
#37206=CARTESIAN_POINT('Ctrl Pts',(-0.146423861786649,-0.0825096309536398,
0.891497316751722));
#37207=CARTESIAN_POINT('Ctrl Pts',(-0.0503376402892206,-0.17681153483915,
0.900004368932038));
#37208=CARTESIAN_POINT('Ctrl Pts',(0.12121644264892,-0.138212772940753,
0.911115533980582));
#37209=CARTESIAN_POINT('Ctrl Pts',(0.181867711471885,0.026839009932345,
0.922226699029127));
#37210=CARTESIAN_POINT('Ctrl Pts',(0.0761253709552246,0.167335367481701,
0.933337864077668));
#37211=CARTESIAN_POINT('Ctrl Pts',(-0.099265255914171,0.154733978795034,
0.944449029126215));
#37212=CARTESIAN_POINT('Ctrl Pts',(-0.155732851093913,0.0517959404958592,
0.951867866913534));
#37213=CARTESIAN_POINT('Ctrl Pts',(-0.155804772838109,0.000161323939398619,
0.955582983018006));
#37214=CARTESIAN_POINT('Ctrl Pts',(-0.155804728476752,2.95821195150548E-6,
0.95559437743963));
#37215=CARTESIAN_POINT('Ctrl Pts',(-0.155794751152569,-3.71416033132616E-5,
0.899405622560372));
#37216=CARTESIAN_POINT('Ctrl Pts',(-0.155801224941728,-0.0020493184051098,
0.899550373830729));
#37217=CARTESIAN_POINT('Ctrl Pts',(-0.154853952527048,-0.055575068168544,
0.903401339095459));
#37218=CARTESIAN_POINT('Ctrl Pts',(-0.0935609375970031,-0.15829679799695,
0.91095851835456));
#37219=CARTESIAN_POINT('Ctrl Pts',(0.0823234386500799,-0.164421340203127,
0.922077160337675));
#37220=CARTESIAN_POINT('Ctrl Pts',(0.182795976495949,-0.0199287985657338,
0.933195802320793));
#37221=CARTESIAN_POINT('Ctrl Pts',(0.115819463928053,0.142819381470141,
0.944314444303908));
#37222=CARTESIAN_POINT('Ctrl Pts',(-0.0572526917402423,0.174738822826618,
0.955433086287024));
#37223=CARTESIAN_POINT('Ctrl Pts',(-0.147990815776177,0.0783419353749631,
0.963796812372513));
#37224=CARTESIAN_POINT('Ctrl Pts',(-0.15563214066504,0.01342816322173,0.968454324463628));
#37225=CARTESIAN_POINT('Ctrl Pts',(-0.155512930646214,0.000141921665610296,
0.969405622560371));
#37226=CARTESIAN_POINT('Origin',(0.,0.,-0.129405622560369));
#37227=CARTESIAN_POINT('',(-0.155333906144275,7.80263919018194E-5,0.815594377439631));
#37228=CARTESIAN_POINT('',(-0.155403083159801,-0.000119596074553197,0.829405622560371));
#37229=CARTESIAN_POINT('',(-0.15555,-2.01987159101623E-14,-0.129405622560369));
#37230=CARTESIAN_POINT('Ctrl Pts',(-0.155333906144275,7.80263919018167E-5,
0.815594377439631));
#37231=CARTESIAN_POINT('Ctrl Pts',(-0.155193217426013,-0.0308862600127516,
0.817804989490498));
#37232=CARTESIAN_POINT('Ctrl Pts',(-0.13122308335565,-0.113929638534857,
0.823719323224213));
#37233=CARTESIAN_POINT('Ctrl Pts',(0.00400949547363229,-0.183793690702293,
0.833337378640777));
#37234=CARTESIAN_POINT('Ctrl Pts',(0.156567267939011,-0.0963477420579929,
0.844448543689319));
#37235=CARTESIAN_POINT('Ctrl Pts',(0.165879203582308,0.0792482593671729,
0.855559708737864));
#37236=CARTESIAN_POINT('Ctrl Pts',(0.0234256671005791,0.182338791618694,
0.866670873786407));
#37237=CARTESIAN_POINT('Ctrl Pts',(-0.124241507899534,0.124912116508194,
0.87668243002033));
#37238=CARTESIAN_POINT('Ctrl Pts',(-0.155154841917538,0.0362716593952071,
0.882990264571404));
#37239=CARTESIAN_POINT('Ctrl Pts',(-0.155453687436568,-0.000133745576774402,
0.885594377439631));
#37240=CARTESIAN_POINT('Ctrl Pts',(-0.155403083159801,-0.000119596074553188,
0.829405622560371));
#37241=CARTESIAN_POINT('Ctrl Pts',(-0.155527408252746,-0.017480188940304,
0.830646423197829));
#37242=CARTESIAN_POINT('Ctrl Pts',(-0.14483135129372,-0.0865473027753662,
0.83559343782966));
#37243=CARTESIAN_POINT('Ctrl Pts',(-0.0434704832044991,-0.178666848096071,
0.844246666455862));
#37244=CARTESIAN_POINT('Ctrl Pts',(0.126590215885116,-0.133365823077974,
0.855365308438979));
#37245=CARTESIAN_POINT('Ctrl Pts',(0.18068878531032,0.0341040818691465,
0.866483950422094));
#37246=CARTESIAN_POINT('Ctrl Pts',(0.069268588294083,0.170333168137465,
0.877602592405212));
#37247=CARTESIAN_POINT('Ctrl Pts',(-0.103328002592178,0.150787500329959,
0.888576483117969));
#37248=CARTESIAN_POINT('Ctrl Pts',(-0.155635469933735,0.0494704907375218,
0.895844159836357));
#37249=CARTESIAN_POINT('Ctrl Pts',(-0.155794751152569,-3.71416033132616E-5,
0.899405622560372));
#37250=CARTESIAN_POINT('Origin',(0.,0.,-0.129405622560369));
#37251=CARTESIAN_POINT('',(-0.155738164088485,9.0367155389158E-5,0.745594377439631));
#37252=CARTESIAN_POINT('',(-0.155363820104426,0.000100737127591941,0.759405622560371));
#37253=CARTESIAN_POINT('',(-0.15555,-2.01987159101623E-14,-0.129405622560369));
#37254=CARTESIAN_POINT('Ctrl Pts',(-0.155738164088485,9.03671553891608E-5,
0.745594377439631));
#37255=CARTESIAN_POINT('Ctrl Pts',(-0.155418612064456,-0.0461276292775272,
0.748915992726744));
#37256=CARTESIAN_POINT('Ctrl Pts',(-0.109121796390773,-0.144436334125619,
0.755941329696705));
#37257=CARTESIAN_POINT('Ctrl Pts',(0.0580004387659595,-0.174448118065669,
0.766670388349515));
#37258=CARTESIAN_POINT('Ctrl Pts',(0.17800908511122,-0.0459234407622611,
0.777781553398057));
#37259=CARTESIAN_POINT('Ctrl Pts',(0.135154441460109,0.124617309179735,
0.788892718446602));
#37260=CARTESIAN_POINT('Ctrl Pts',(-0.0313551099181417,0.181143738163968,
0.800003883495145));
#37261=CARTESIAN_POINT('Ctrl Pts',(-0.141757073229054,0.0936656796997624,
0.808904436492822));
#37262=CARTESIAN_POINT('Ctrl Pts',(-0.155428931266511,0.0209921774117757,
0.81410126780765));
#37263=CARTESIAN_POINT('Ctrl Pts',(-0.155333906144275,7.80263919018167E-5,
0.815594377439631));
#37264=CARTESIAN_POINT('Ctrl Pts',(-0.155363820104426,0.000100737127591942,
0.759405622560371));
#37265=CARTESIAN_POINT('Ctrl Pts',(-0.155169765832855,-0.0326159426902871,
0.76174247256493));
#37266=CARTESIAN_POINT('Ctrl Pts',(-0.129071878250434,-0.117503987929593,
0.767785536563862));
#37267=CARTESIAN_POINT('Ctrl Pts',(0.0103792628149562,-0.18358593744105,
0.777534814557165));
#37268=CARTESIAN_POINT('Ctrl Pts',(0.159909575810308,-0.0907769413831382,
0.78865345654028));
#37269=CARTESIAN_POINT('Ctrl Pts',(0.162955779866738,0.0851876712390422,
0.799772098523398));
#37270=CARTESIAN_POINT('Ctrl Pts',(0.0167274199086701,0.183116681231986,
0.810890740506512));
#37271=CARTESIAN_POINT('Ctrl Pts',(-0.126795424285233,0.121093838634352,
0.820768581852172));
#37272=CARTESIAN_POINT('Ctrl Pts',(-0.155156054962447,0.0343750973057136,
0.826940209203457));
#37273=CARTESIAN_POINT('Ctrl Pts',(-0.155403083159801,-0.000119596074553188,
0.829405622560371));
#37274=CARTESIAN_POINT('Origin',(0.,0.,-0.129405622560369));
#37275=CARTESIAN_POINT('',(-0.155606466149984,-0.000136591087330588,0.67559437743963));
#37276=CARTESIAN_POINT('',(-0.155769406638298,6.77585252333857E-5,0.689405622560371));
#37277=CARTESIAN_POINT('',(-0.15555,-2.01987159101623E-14,-0.129405622560369));
#37278=CARTESIAN_POINT('Ctrl Pts',(-0.155606466149984,-0.000136591087330577,
0.67559437743963));
#37279=CARTESIAN_POINT('Ctrl Pts',(-0.155699698050756,-0.010301028373747,
0.676323274280142));
#37280=CARTESIAN_POINT('Ctrl Pts',(-0.150160999329305,-0.0720125819190329,
0.680755892803501));
#37281=CARTESIAN_POINT('Ctrl Pts',(-0.0677079673289082,-0.170914680334463,
0.68889223300971));
#37282=CARTESIAN_POINT('Ctrl Pts',(0.106838781720774,-0.149605051766532,
0.700003398058251));
#37283=CARTESIAN_POINT('Ctrl Pts',(0.183637062036826,0.00858057341481814,
0.711114563106797));
#37284=CARTESIAN_POINT('Ctrl Pts',(0.0924229284360449,0.1589156980696,0.722225728155339));
#37285=CARTESIAN_POINT('Ctrl Pts',(-0.0833503847528551,0.163856370505402,
0.733336893203883));
#37286=CARTESIAN_POINT('Ctrl Pts',(-0.153115801604342,0.0622214122864029,
0.741126442965314));
#37287=CARTESIAN_POINT('Ctrl Pts',(-0.155774924177056,0.00540711533618156,
0.745212271043896));
#37288=CARTESIAN_POINT('Ctrl Pts',(-0.155738164088485,9.03671553891608E-5,
0.745594377439631));
#37289=CARTESIAN_POINT('Ctrl Pts',(-0.155769406638298,6.77585252333878E-5,
0.689405622560371));
#37290=CARTESIAN_POINT('Ctrl Pts',(-0.155508734647919,-0.0476733936548398,
0.692838521932031));
#37291=CARTESIAN_POINT('Ctrl Pts',(-0.106472330039144,-0.147419539900055,
0.699977635298063));
#37292=CARTESIAN_POINT('Ctrl Pts',(0.0633314188332071,-0.172628667698419,
0.710822962658467));
#37293=CARTESIAN_POINT('Ctrl Pts',(0.17940008868909,-0.0403377453646542,
0.721941604641583));
#37294=CARTESIAN_POINT('Ctrl Pts',(0.131130494233742,0.128904301731096,
0.733060246624699));
#37295=CARTESIAN_POINT('Ctrl Pts',(-0.0372603218894873,0.180064416072257,
0.744178888607816));
#37296=CARTESIAN_POINT('Ctrl Pts',(-0.143301362666466,0.0901927254173143,
0.752960680586373));
#37297=CARTESIAN_POINT('Ctrl Pts',(-0.155477533406966,0.0192722899107996,
0.758036258570558));
#37298=CARTESIAN_POINT('Ctrl Pts',(-0.155363820104426,0.000100737127591942,
0.759405622560371));
#37299=CARTESIAN_POINT('Origin',(0.,0.,-0.129405622560369));
#37300=CARTESIAN_POINT('',(-0.155295085115974,-2.74912889200857E-6,0.60559437743963));
#37301=CARTESIAN_POINT('',(-0.155567057787938,-0.000141549514015751,0.619405622560371));
#37302=CARTESIAN_POINT('',(-0.15555,-2.01987159101623E-14,-0.129405622560369));
#37303=CARTESIAN_POINT('Ctrl Pts',(-0.155295114066544,-2.74881667468134E-6,
0.60559437743963));
#37304=CARTESIAN_POINT('Ctrl Pts',(-0.155299180574127,-0.0257905198155464,
0.607434277516388));
#37305=CARTESIAN_POINT('Ctrl Pts',(-0.137005956536857,-0.103483686203599,
0.612977899275993));
#37306=CARTESIAN_POINT('Ctrl Pts',(-0.0143272298638598,-0.183278278249422,
0.622225242718446));
#37307=CARTESIAN_POINT('Ctrl Pts',(0.146185859526926,-0.111471481859797,
0.63333640776699));
#37308=CARTESIAN_POINT('Ctrl Pts',(0.172951224644592,0.0623223129190563,
0.644447572815534));
#37309=CARTESIAN_POINT('Ctrl Pts',(0.0414808152398764,0.179096450999678,
0.655558737864077));
#37310=CARTESIAN_POINT('Ctrl Pts',(-0.11682689842466,0.135101180160119,
0.66594100607211));
#37311=CARTESIAN_POINT('Ctrl Pts',(-0.155225961585962,0.0413472223515983,
0.672619552597294));
#37312=CARTESIAN_POINT('Ctrl Pts',(-0.155606466149984,-0.000136591087330577,
0.67559437743963));
#37313=CARTESIAN_POINT('Ctrl Pts',(-0.155567057787938,-0.000141549514015748,
0.619405622560371));
#37314=CARTESIAN_POINT('Ctrl Pts',(-0.155673152840384,-0.011622012238534,
0.62022835730476));
#37315=CARTESIAN_POINT('Ctrl Pts',(-0.149271086742403,-0.0747018195902368,
0.62475730604352));
#37316=CARTESIAN_POINT('Ctrl Pts',(-0.0632665469493242,-0.172652453095426,
0.632992468776653));
#37317=CARTESIAN_POINT('Ctrl Pts',(0.110806726459172,-0.146742614445027,
0.644111110759769));
#37318=CARTESIAN_POINT('Ctrl Pts',(0.183376231205259,0.0135898253011021,
0.655229752742886));
#37319=CARTESIAN_POINT('Ctrl Pts',(0.0879651525947856,0.161473395492061,
0.666348394726001));
#37320=CARTESIAN_POINT('Ctrl Pts',(-0.0880258220622017,0.161440330069759,
0.677467036709119));
#37321=CARTESIAN_POINT('Ctrl Pts',(-0.153940153309356,0.0591912849892102,
0.685152779320574));
#37322=CARTESIAN_POINT('Ctrl Pts',(-0.155790160368306,0.00386873070159844,
0.689132307937659));
#37323=CARTESIAN_POINT('Ctrl Pts',(-0.155769406638298,6.77585252333878E-5,
0.689405622560371));
#37324=CARTESIAN_POINT('Origin',(0.,0.,-0.129405622560369));
#37325=CARTESIAN_POINT('',(-0.155596383579478,0.000138071545366175,0.53559437743963));
#37326=CARTESIAN_POINT('',(-0.15529563387483,1.51106445085702E-5,0.549405622560371));
#37327=CARTESIAN_POINT('',(-0.15555,-2.01987159101623E-14,-0.129405622560369));
#37328=CARTESIAN_POINT('Ctrl Pts',(-0.155596383579478,0.000138071545366179,
0.53559437743963));
#37329=CARTESIAN_POINT('Ctrl Pts',(-0.155217514150148,-0.0410190199764792,
0.538545280752634));
#37330=CARTESIAN_POINT('Ctrl Pts',(-0.117330640529453,-0.134449549172498,
0.545199905748485));
#37331=CARTESIAN_POINT('Ctrl Pts',(0.0403262995152723,-0.179359935217008,
0.555558252427184));
#37332=CARTESIAN_POINT('Ctrl Pts',(0.172546185411942,-0.0634350903950841,
0.566669417475728));
#37333=CARTESIAN_POINT('Ctrl Pts',(0.146900873501267,0.11052750860401,0.577780582524271));
#37334=CARTESIAN_POINT('Ctrl Pts',(-0.013146340126236,0.183366765077345,
0.588891747572816));
#37335=CARTESIAN_POINT('Ctrl Pts',(-0.136655195880861,0.104159698732297,
0.598163012544601));
#37336=CARTESIAN_POINT('Ctrl Pts',(-0.155290994688111,0.0261203028467153,
0.60373055583354));
#37337=CARTESIAN_POINT('Ctrl Pts',(-0.155295114066544,-2.74881667468134E-6,
0.60559437743963));
#37338=CARTESIAN_POINT('Ctrl Pts',(-0.15529563387483,1.51106445085633E-5,
0.549405622560371));
#37339=CARTESIAN_POINT('Ctrl Pts',(-0.155272340811799,-0.0268780222436924,
0.55132440667186));
#37340=CARTESIAN_POINT('Ctrl Pts',(-0.135831396530156,-0.105747938365068,
0.556949404777722));
#37341=CARTESIAN_POINT('Ctrl Pts',(-0.0103102773360761,-0.183589824620028,
0.566280616877956));
#37342=CARTESIAN_POINT('Ctrl Pts',(0.14869956060099,-0.108166382022474,
0.577399258861071));
#37343=CARTESIAN_POINT('Ctrl Pts',(0.171494149863546,0.0663421591850832,
0.588517900844189));
#37344=CARTESIAN_POINT('Ctrl Pts',(0.0371926577693494,0.180078404398782,
0.599636542827304));
#37345=CARTESIAN_POINT('Ctrl Pts',(-0.118720103315053,0.132645343006727,
0.609932450066032));
#37346=CARTESIAN_POINT('Ctrl Pts',(-0.155195221197423,0.040094597399841,
0.616522143310387));
#37347=CARTESIAN_POINT('Ctrl Pts',(-0.155567057787938,-0.000141549514015748,
0.619405622560371));
#37348=CARTESIAN_POINT('Origin',(0.,0.,-0.129405622560369));
#37349=CARTESIAN_POINT('',(-0.155745492001379,-8.56371120316567E-5,0.46559437743963));
#37350=CARTESIAN_POINT('',(-0.155622585425313,0.000134239099646036,0.479405622560371));
#37351=CARTESIAN_POINT('',(-0.15555,-2.01987159101623E-14,-0.129405622560369));
#37352=CARTESIAN_POINT('Ctrl Pts',(-0.155745492001379,-8.56371120316864E-5,
0.465594377439631));
#37353=CARTESIAN_POINT('Ctrl Pts',(-0.15577850741697,-0.00506891626144068,
0.465952562306032));
#37354=CARTESIAN_POINT('Ctrl Pts',(-0.153301192978291,-0.0615473136307116,
0.470014468855281));
#37355=CARTESIAN_POINT('Ctrl Pts',(-0.0844041411881997,-0.163316067010957,
0.477780097087378));
#37356=CARTESIAN_POINT('Ctrl Pts',(0.0913973507436636,-0.159507746114991,
0.488891262135923));
#37357=CARTESIAN_POINT('Ctrl Pts',(0.183577980123458,-0.00976329900371924,
0.500002427184466));
#37358=CARTESIAN_POINT('Ctrl Pts',(0.10780025055099,0.148913742733129,0.51111359223301));
#37359=CARTESIAN_POINT('Ctrl Pts',(-0.0666056105926533,0.17134727727987,
0.522224757281553));
#37360=CARTESIAN_POINT('Ctrl Pts',(-0.149938299705611,0.0726891414718789,
0.530385019017093));
#37361=CARTESIAN_POINT('Ctrl Pts',(-0.155693038683329,0.0106378444150779,
0.534841559069786));
#37362=CARTESIAN_POINT('Ctrl Pts',(-0.155596383579478,0.000138071545366179,
0.53559437743963));
#37363=CARTESIAN_POINT('Ctrl Pts',(-0.155622585425313,0.000134239099646029,
0.479405622560371));
#37364=CARTESIAN_POINT('Ctrl Pts',(-0.155239700220769,-0.0418962472451577,
0.482420456038961));
#37365=CARTESIAN_POINT('Ctrl Pts',(-0.115964303797854,-0.136226320639006,
0.489141503511923));
#37366=CARTESIAN_POINT('Ctrl Pts',(0.0435376164803608,-0.17865050090601,
0.499568764979258));
#37367=CARTESIAN_POINT('Ctrl Pts',(0.173732980498774,-0.0602360109052031,
0.510687406962374));
#37368=CARTESIAN_POINT('Ctrl Pts',(0.144781397169404,0.113357278356683,
0.521806048945491));
#37369=CARTESIAN_POINT('Ctrl Pts',(-0.0167962271460079,0.183110382765203,
0.532924690928607));
#37370=CARTESIAN_POINT('Ctrl Pts',(-0.137758975876034,0.102035875886683,
0.542124548800234));
#37371=CARTESIAN_POINT('Ctrl Pts',(-0.155317332364345,0.0250672199885809,
0.547618192677488));
#37372=CARTESIAN_POINT('Ctrl Pts',(-0.15529563387483,1.51106445085633E-5,
0.549405622560371));
#37373=CARTESIAN_POINT('Origin',(0.,0.,-0.129405622560369));
#37374=CARTESIAN_POINT('',(-0.155339129538237,-8.2587420025254E-5,0.39559437743963));
#37375=CARTESIAN_POINT('',(-0.15573160577951,-9.4952305265919E-5,0.409405622560371));
#37376=CARTESIAN_POINT('',(-0.15555,-2.01987159101623E-14,-0.129405622560369));
#37377=CARTESIAN_POINT('Ctrl Pts',(-0.155339129538237,-8.25874200252562E-5,
0.39559437743963));
#37378=CARTESIAN_POINT('Ctrl Pts',(-0.155438295724494,-0.0206599346759669,
0.397063565542278));
#37379=CARTESIAN_POINT('Ctrl Pts',(-0.142062281789543,-0.0929876204718288,
0.402236475327773));
#37380=CARTESIAN_POINT('Ctrl Pts',(-0.0325213021862407,-0.180938005122649,
0.411113106796117));
#37381=CARTESIAN_POINT('Ctrl Pts',(0.134348911316817,-0.125485325124609,
0.42222427184466));
#37382=CARTESIAN_POINT('Ctrl Pts',(0.178301209192838,0.0447758371671112,
0.433335436893204));
#37383=CARTESIAN_POINT('Ctrl Pts',(0.0591229481908682,0.174070887258225,
0.444446601941748));
#37384=CARTESIAN_POINT('Ctrl Pts',(-0.10856218085317,0.145071736103991,
0.455199582123889));
#37385=CARTESIAN_POINT('Ctrl Pts',(-0.155437119708937,0.0464594445617744,
0.462248840623184));
#37386=CARTESIAN_POINT('Ctrl Pts',(-0.155745492001379,-8.56371120316864E-5,
0.465594377439631));
#37387=CARTESIAN_POINT('Ctrl Pts',(-0.15573160577951,-9.49523052659442E-5,
0.40940562256037));
#37388=CARTESIAN_POINT('Ctrl Pts',(-0.155772052747877,-0.00572626470532979,
0.40981029141169));
#37389=CARTESIAN_POINT('Ctrl Pts',(-0.152938259291224,-0.0628915705084586,
0.413921174257381));
#37390=CARTESIAN_POINT('Ctrl Pts',(-0.0822616502622442,-0.164452261823584,
0.421738271097444));
#37391=CARTESIAN_POINT('Ctrl Pts',(0.0936204134582059,-0.158261630557358,
0.43285691308056));
#37392=CARTESIAN_POINT('Ctrl Pts',(0.183742116834086,-0.00709647969689106,
0.443975555063676));
#37393=CARTESIAN_POINT('Ctrl Pts',(0.10554806974386,0.150569354438759,0.455094197046793));
#37394=CARTESIAN_POINT('Ctrl Pts',(-0.0693325883166112,0.170307127625589,
0.466212839029909));
#37395=CARTESIAN_POINT('Ctrl Pts',(-0.150503746143118,0.0709862178387775,
0.474316647534435));
#37396=CARTESIAN_POINT('Ctrl Pts',(-0.155710391061042,0.00977293375193425,
0.478714242044589));
#37397=CARTESIAN_POINT('Ctrl Pts',(-0.155622585425313,0.000134239099646029,
0.479405622560371));
#37398=CARTESIAN_POINT('Origin',(0.,0.,-0.129405622560369));
#37399=CARTESIAN_POINT('',(-0.155444674488022,0.000131742778884735,0.32559437743963));
#37400=CARTESIAN_POINT('',(-0.15533186684889,-7.70198572060954E-5,0.339405622560371));
#37401=CARTESIAN_POINT('',(-0.15555,-2.01987159101623E-14,-0.129405622560369));
#37402=CARTESIAN_POINT('Ctrl Pts',(-0.155444674488022,0.000131742778884739,
0.32559437743963));
#37403=CARTESIAN_POINT('Ctrl Pts',(-0.155154236665719,-0.0359445316439912,
0.328174568778523));
#37404=CARTESIAN_POINT('Ctrl Pts',(-0.124691611905359,-0.124248704432008,
0.334458481800264));
#37405=CARTESIAN_POINT('Ctrl Pts',(0.0222506403513669,-0.18248590575151,
0.344446116504855));
#37406=CARTESIAN_POINT('Ctrl Pts',(0.165365282072159,-0.0803151310699741,
0.355557281553397));
#37407=CARTESIAN_POINT('Ctrl Pts',(0.157184646516792,0.0953372104320743,
0.366668446601942));
#37408=CARTESIAN_POINT('Ctrl Pts',(0.00519332482321354,0.183764050268212,
0.377779611650485));
#37409=CARTESIAN_POINT('Ctrl Pts',(-0.130823935507303,0.114600960175539,
0.387421588596382));
#37410=CARTESIAN_POINT('Ctrl Pts',(-0.155188304621527,0.0312141358191517,
0.39335984385943));
#37411=CARTESIAN_POINT('Ctrl Pts',(-0.155339129538237,-8.25874200252562E-5,
0.39559437743963));
#37412=CARTESIAN_POINT('Ctrl Pts',(-0.15533186684889,-7.70198572060919E-5,
0.339405622560371));
#37413=CARTESIAN_POINT('Ctrl Pts',(-0.155425971941861,-0.0210984061911746,
0.34090634077879));
#37414=CARTESIAN_POINT('Ctrl Pts',(-0.141654850766895,-0.0939166341982764,
0.346113272991582));
#37415=CARTESIAN_POINT('Ctrl Pts',(-0.0308692884081366,-0.181269447386996,
0.355026419198746));
#37416=CARTESIAN_POINT('Ctrl Pts',(0.135606994996762,-0.124186426112907,
0.366145061181863));
#37417=CARTESIAN_POINT('Ctrl Pts',(0.177861387826841,0.0466567491694538,
0.377263703164979));
#37418=CARTESIAN_POINT('Ctrl Pts',(0.0571870330903418,0.174760318061885,
0.388382345148095));
#37419=CARTESIAN_POINT('Ctrl Pts',(-0.109574509035902,0.143939945308724,
0.399096318279893));
#37420=CARTESIAN_POINT('Ctrl Pts',(-0.155401613758806,0.0458488658137791,
0.406104077417318));
#37421=CARTESIAN_POINT('Ctrl Pts',(-0.15573160577951,-9.49523052659442E-5,
0.40940562256037));
#37422=CARTESIAN_POINT('Origin',(0.,0.,-0.129405622560369));
#37423=CARTESIAN_POINT('',(-0.155804712705668,3.25009013604671E-6,0.25559437743963));
#37424=CARTESIAN_POINT('',(-0.155449947323643,0.000133480041304715,0.269405622560371));
#37425=CARTESIAN_POINT('',(-0.15555,-2.01987159101623E-14,-0.129405622560369));
#37426=CARTESIAN_POINT('Ctrl Pts',(-0.155804712705668,3.25009013604029E-6,
0.25559437743963));
#37427=CARTESIAN_POINT('Ctrl Pts',(-0.155788927539753,-0.0512989453804214,
0.259285572014769));
#37428=CARTESIAN_POINT('Ctrl Pts',(-0.10006227616332,-0.154106832868198,
0.266680488272757));
#37429=CARTESIAN_POINT('Ctrl Pts',(0.0750458968510211,-0.167822257683237,
0.277779126213592));
#37430=CARTESIAN_POINT('Ctrl Pts',(0.181691053470019,-0.0280099604209337,
0.288890291262136));
#37431=CARTESIAN_POINT('Ctrl Pts',(0.122104229764526,0.137429086670804,
0.30000145631068));
#37432=CARTESIAN_POINT('Ctrl Pts',(-0.0491976593161155,0.177132117679823,
0.311112621359223));
#37433=CARTESIAN_POINT('Ctrl Pts',(-0.146161229246342,0.0831876851886141,
0.319643595068874));
#37434=CARTESIAN_POINT('Ctrl Pts',(-0.155571144064704,0.0158409610837222,
0.324470847095676));
#37435=CARTESIAN_POINT('Ctrl Pts',(-0.155444674488022,0.000131742778884739,
0.32559437743963));
#37436=CARTESIAN_POINT('Ctrl Pts',(-0.155449947323643,0.000133480041304701,
0.269405622560371));
#37437=CARTESIAN_POINT('Ctrl Pts',(-0.155153406972295,-0.0361714100102126,
0.272002390145891));
#37438=CARTESIAN_POINT('Ctrl Pts',(-0.12437032104418,-0.124745277135715,
0.278305371725784));
#37439=CARTESIAN_POINT('Ctrl Pts',(0.0231926238140432,-0.182410602009977,
0.288314567300049));
#37440=CARTESIAN_POINT('Ctrl Pts',(0.165866396469461,-0.0793716828903688,
0.299433209283165));
#37441=CARTESIAN_POINT('Ctrl Pts',(0.156599354026699,0.096375141196464,
0.310551851266282));
#37442=CARTESIAN_POINT('Ctrl Pts',(0.00388050940998321,0.183838154825996,
0.321670493249398));
#37443=CARTESIAN_POINT('Ctrl Pts',(-0.131300314367493,0.113822266482633,
0.331288417014094));
#37444=CARTESIAN_POINT('Ctrl Pts',(-0.155193567478298,0.0308165737536199,
0.337200126784418));
#37445=CARTESIAN_POINT('Ctrl Pts',(-0.15533186684889,-7.70198572060919E-5,
0.339405622560371));
#37446=CARTESIAN_POINT('Origin',(0.,0.,-0.129405622560369));
#37447=CARTESIAN_POINT('',(-0.155454118234884,-0.000133834695600709,0.18559437743963));
#37448=CARTESIAN_POINT('',(-0.155805467550008,3.4854191793785E-6,0.19940562256037));
#37449=CARTESIAN_POINT('',(-0.15555,-2.01987159101623E-14,-0.129405622560369));
#37450=CARTESIAN_POINT('Ctrl Pts',(-0.155454118234884,-0.000133834695600729,
0.18559437743963));
#37451=CARTESIAN_POINT('Ctrl Pts',(-0.155580288786201,-0.0154903851691022,
0.186692853568168));
#37452=CARTESIAN_POINT('Ctrl Pts',(-0.146436232298065,-0.0824775316270878,
0.191495051379553));
#37453=CARTESIAN_POINT('Ctrl Pts',(-0.0503915664640746,-0.176796168665343,
0.200000970873786));
#37454=CARTESIAN_POINT('Ctrl Pts',(0.121174280763407,-0.138249741391359,
0.21111213592233));
#37455=CARTESIAN_POINT('Ctrl Pts',(0.181875888824183,0.0267835396201195,
0.222223300970874));
#37456=CARTESIAN_POINT('Ctrl Pts',(0.0761764071097843,0.167312138149853,
0.233334466019417));
#37457=CARTESIAN_POINT('Ctrl Pts',(-0.0992180579104728,0.154764252547341,
0.244445631067961));
#37458=CARTESIAN_POINT('Ctrl Pts',(-0.155725669913861,0.0518277207581445,
0.251865601541365));
#37459=CARTESIAN_POINT('Ctrl Pts',(-0.155804766277071,0.00017735852989955,
0.255581850331921));
#37460=CARTESIAN_POINT('Ctrl Pts',(-0.155804712705668,3.25009013604029E-6,
0.25559437743963));
#37461=CARTESIAN_POINT('Ctrl Pts',(-0.155805467550008,3.48541917938314E-6,
0.19940562256037));
#37462=CARTESIAN_POINT('Ctrl Pts',(-0.155788564535512,-0.0513206116891616,
0.203098439512992));
#37463=CARTESIAN_POINT('Ctrl Pts',(-0.100003893378143,-0.154186484140614,
0.210497470459985));
#37464=CARTESIAN_POINT('Ctrl Pts',(0.0752488571272716,-0.167777039880966,
0.221602715401351));
#37465=CARTESIAN_POINT('Ctrl Pts',(0.181781810074028,-0.0276929424335053,
0.232721357384467));
#37466=CARTESIAN_POINT('Ctrl Pts',(0.121794738393109,0.137759091140133,
0.243839999367584));
#37467=CARTESIAN_POINT('Ctrl Pts',(-0.0497615974795104,0.177017821004958,
0.2549586413507));
#37468=CARTESIAN_POINT('Ctrl Pts',(-0.146313162187878,0.0828233020270418,
0.263480515748296));
#37469=CARTESIAN_POINT('Ctrl Pts',(-0.155576641614544,0.0156444291597347,
0.268296176151519));
#37470=CARTESIAN_POINT('Ctrl Pts',(-0.155449947323643,0.000133480041304701,
0.269405622560371));
#37471=CARTESIAN_POINT('Origin',(0.,0.,-0.129405622560369));
#37472=CARTESIAN_POINT('',(-0.155333634177863,7.79921548230329E-5,0.11559437743963));
#37473=CARTESIAN_POINT('',(-0.155460191805193,-0.000135568056800359,0.12940562256037));
#37474=CARTESIAN_POINT('',(-0.15555,-2.01987159101623E-14,-0.129405622560369));
#37475=CARTESIAN_POINT('Ctrl Pts',(-0.155333634177863,7.79921548230561E-5,
0.11559437743963));
#37476=CARTESIAN_POINT('Ctrl Pts',(-0.155193438638927,-0.0308706275100063,
0.117803856804414));
#37477=CARTESIAN_POINT('Ctrl Pts',(-0.131241956589738,-0.11389814578602,
0.123717057852045));
#37478=CARTESIAN_POINT('Ctrl Pts',(0.00395347168138628,-0.183794704008407,
0.133333980582524));
#37479=CARTESIAN_POINT('Ctrl Pts',(0.156537855283131,-0.0963955976349113,
0.144445145631068));
#37480=CARTESIAN_POINT('Ctrl Pts',(0.165903376979378,0.0791977165381959,
0.155556310679611));
#37481=CARTESIAN_POINT('Ctrl Pts',(0.0234812759114929,0.182331608910266,
0.166667475728155));
#37482=CARTESIAN_POINT('Ctrl Pts',(-0.124220109658982,0.124943524423025,
0.176680164648161));
#37483=CARTESIAN_POINT('Ctrl Pts',(-0.155154880719052,0.0362871523529771,
0.18298913188532));
#37484=CARTESIAN_POINT('Ctrl Pts',(-0.155454118234884,-0.000133834695600729,
0.18559437743963));
#37485=CARTESIAN_POINT('Ctrl Pts',(-0.155460191805193,-0.000135568056800364,
0.12940562256037));
#37486=CARTESIAN_POINT('Ctrl Pts',(-0.15558637635503,-0.0152693971168416,
0.130488274885721));
#37487=CARTESIAN_POINT('Ctrl Pts',(-0.146605510259419,-0.0820638709603335,
0.135277141205443));
#37488=CARTESIAN_POINT('Ctrl Pts',(-0.0510374815939226,-0.176654153931159,
0.143772221519537));
#37489=CARTESIAN_POINT('Ctrl Pts',(0.120797626960931,-0.138634273102519,
0.154890863502654));
#37490=CARTESIAN_POINT('Ctrl Pts',(0.181976886629041,0.0263806680570579,
0.16600950548577));
#37491=CARTESIAN_POINT('Ctrl Pts',(0.0764574137846417,0.167229745635935,
0.177128147468886));
#37492=CARTESIAN_POINT('Ctrl Pts',(-0.0991003621173195,0.154889135395602,
0.188246789452002));
#37493=CARTESIAN_POINT('Ctrl Pts',(-0.15572087700955,0.0518861158146895,
0.195672614482497));
#37494=CARTESIAN_POINT('Ctrl Pts',(-0.155805528871865,0.000189682319971778,
0.19939222551862));
#37495=CARTESIAN_POINT('Ctrl Pts',(-0.155805467550008,3.48541917938314E-6,
0.19940562256037));
#37496=CARTESIAN_POINT('Origin',(0.,0.,-0.129405622560369));
#37497=CARTESIAN_POINT('',(-0.155735926886437,0.000101346774827271,0.0455943774396301));
#37498=CARTESIAN_POINT('',(-0.155326046963413,7.29270061605516E-5,0.0594056225603705));
#37499=CARTESIAN_POINT('',(-0.15555,-2.01987159101623E-14,-0.129405622560369));
#37500=CARTESIAN_POINT('Ctrl Pts',(-0.155735926886437,0.000101346774827265,
0.0455943774396301));
#37501=CARTESIAN_POINT('Ctrl Pts',(-0.15541538777776,-0.0460983628495037,
0.0489148600406595));
#37502=CARTESIAN_POINT('Ctrl Pts',(-0.109151218308356,-0.144423481489054,
0.0559390643245367));
#37503=CARTESIAN_POINT('Ctrl Pts',(0.0579488995883613,-0.174456230311225,
0.0666669902912619));
#37504=CARTESIAN_POINT('Ctrl Pts',(0.177994191588978,-0.0459827600750814,
0.0777781553398056));
#37505=CARTESIAN_POINT('Ctrl Pts',(0.135192905881154,0.124578720765632,
0.0888893203883492));
#37506=CARTESIAN_POINT('Ctrl Pts',(-0.0313001003158473,0.181151906168851,
0.100000485436893));
#37507=CARTESIAN_POINT('Ctrl Pts',(-0.141742497137191,0.093698092273704,
0.108902171120653));
#37508=CARTESIAN_POINT('Ctrl Pts',(-0.155428446607623,0.0210081433596544,
0.114100135121566));
#37509=CARTESIAN_POINT('Ctrl Pts',(-0.155333634177863,7.79921548230561E-5,
0.11559437743963));
#37510=CARTESIAN_POINT('Ctrl Pts',(-0.155326046963413,7.29270061605551E-5,
0.0594056225603705));
#37511=CARTESIAN_POINT('Ctrl Pts',(-0.155199262831984,-0.0304485333833814,
0.0615843242528215));
#37512=CARTESIAN_POINT('Ctrl Pts',(-0.131743653601245,-0.113071739766558,
0.0674692399396446));
#37513=CARTESIAN_POINT('Ctrl Pts',(0.00255447675030308,-0.183860034663711,
0.0770603696208398));
#37514=CARTESIAN_POINT('Ctrl Pts',(0.155899683301632,-0.0975032021788082,
0.0881790116039561));
#37515=CARTESIAN_POINT('Ctrl Pts',(0.166434877052597,0.0781732535368643,
0.0992976535870723));
#37516=CARTESIAN_POINT('Ctrl Pts',(0.0245080507541896,0.182238325373942,
0.110416295570189));
#37517=CARTESIAN_POINT('Ctrl Pts',(-0.123863138927055,0.125487925833816,
0.120452285227955));
#37518=CARTESIAN_POINT('Ctrl Pts',(-0.155154412248428,0.0365378245899198,
0.126782060891349));
#37519=CARTESIAN_POINT('Ctrl Pts',(-0.155460191805193,-0.000135568056800364,
0.12940562256037));
#37520=CARTESIAN_POINT('Origin',(0.,0.,1.15));
#37521=CARTESIAN_POINT('',(-0.177892626630995,-0.00012009523392913,1.12223275485995));
#37522=CARTESIAN_POINT('Ctrl Pts',(0.155548765964692,0.000619602180104872,
1.14445));
#37523=CARTESIAN_POINT('Ctrl Pts',(0.156083861551471,-0.0102125174737046,
1.14395805623115));
#37524=CARTESIAN_POINT('Ctrl Pts',(0.15539846640382,-0.0210404421466269,
1.14347026853365));
#37525=CARTESIAN_POINT('Ctrl Pts',(0.153608590638952,-0.0317127652002419,
1.14298392615444));
#37526=CARTESIAN_POINT('Ctrl Pts',(0.152914716720618,-0.0358500616318106,
1.14279538776594));
#37527=CARTESIAN_POINT('Ctrl Pts',(0.152054287987853,-0.0399640361908485,
1.14260706658696));
#37528=CARTESIAN_POINT('Ctrl Pts',(0.151032028551573,-0.0440458121014301,
1.1424188046881));
#37529=CARTESIAN_POINT('Ctrl Pts',(0.150071136707034,-0.0478825535826186,
1.14224184440107));
#37530=CARTESIAN_POINT('Ctrl Pts',(0.148969254907822,-0.0516824965112672,
1.14206531990211));
#37531=CARTESIAN_POINT('Ctrl Pts',(0.147732675525468,-0.0554351396328931,
1.14188926057926));
#37532=CARTESIAN_POINT('Ctrl Pts',(0.144705099540774,-0.0646229138722882,
1.14145820618411));
#37533=CARTESIAN_POINT('Ctrl Pts',(0.14087037084284,-0.0735342808861364,
1.14102963880076));
#37534=CARTESIAN_POINT('Ctrl Pts',(0.136287966367236,-0.0820616333277537,
1.14060170770949));
#37535=CARTESIAN_POINT('Ctrl Pts',(0.134099734044687,-0.0861336938230361,
1.1403973580824));
#37536=CARTESIAN_POINT('Ctrl Pts',(0.131738457084688,-0.090120565054425,
1.14019301071694));
#37537=CARTESIAN_POINT('Ctrl Pts',(0.129223539536337,-0.0939888668888786,
1.1399895855729));
#37538=CARTESIAN_POINT('Ctrl Pts',(0.123841150615535,-0.102267748615928,
1.1395542181223));
#37539=CARTESIAN_POINT('Ctrl Pts',(0.117747056171278,-0.110025200831312,
1.1391220629978));
#37540=CARTESIAN_POINT('Ctrl Pts',(0.11100116606729,-0.117148456023219,
1.13869123413476));
#37541=CARTESIAN_POINT('Ctrl Pts',(0.106906026602935,-0.121472677586479,
1.13842969647966));
#37542=CARTESIAN_POINT('Ctrl Pts',(0.102570142764087,-0.125562999006382,
1.13816864757596));
#37543=CARTESIAN_POINT('Ctrl Pts',(0.0980025572591369,-0.129390839920029,
1.13790766548932));
#37544=CARTESIAN_POINT('Ctrl Pts',(0.0956731876101781,-0.131342955854285,
1.13777457027942));
#37545=CARTESIAN_POINT('Ctrl Pts',(0.0932817165779503,-0.133228060285772,
1.13764139558094));
#37546=CARTESIAN_POINT('Ctrl Pts',(0.0908350990518728,-0.135037587415829,
1.1375084117344));
#37547=CARTESIAN_POINT('Ctrl Pts',(0.0901763381324703,-0.135524809363345,
1.13747260533636));
#37548=CARTESIAN_POINT('Ctrl Pts',(0.0895137718121014,-0.136006421121091,
1.1374368229172));
#37549=CARTESIAN_POINT('Ctrl Pts',(0.0888474357058895,-0.136482361432558,
1.13740106343829));
#37550=CARTESIAN_POINT('Ctrl Pts',(0.0798411198483208,-0.142915254284167,
1.1369177320399));
#37551=CARTESIAN_POINT('Ctrl Pts',(0.0701492813036541,-0.148315340119806,
1.1364385915245));
#37552=CARTESIAN_POINT('Ctrl Pts',(0.059971176200061,-0.152699426079087,
1.13596107719954));
#37553=CARTESIAN_POINT('Ctrl Pts',(0.0530631196487977,-0.155674981295315,
1.13563697994103));
#37554=CARTESIAN_POINT('Ctrl Pts',(0.0459300802687867,-0.158181722966519,
1.13531363179894));
#37555=CARTESIAN_POINT('Ctrl Pts',(0.0386275637501033,-0.16021396300419,
1.13499023090658));
#37556=CARTESIAN_POINT('Ctrl Pts',(0.0351988940876516,-0.161168138149998,
1.13483838806916));
#37557=CARTESIAN_POINT('Ctrl Pts',(0.0317324236549294,-0.162017357570902,
1.13468652012024));
#37558=CARTESIAN_POINT('Ctrl Pts',(0.028249074324747,-0.162757963065587,
1.13453519958799));
#37559=CARTESIAN_POINT('Ctrl Pts',(0.0167982212800381,-0.165192563755867,
1.13403776191718));
#37560=CARTESIAN_POINT('Ctrl Pts',(0.00512774808450533,-0.166468890755321,
1.13354451715097));
#37561=CARTESIAN_POINT('Ctrl Pts',(-0.00655533748915361,-0.166579173106486,
1.13305265956701));
#37562=CARTESIAN_POINT('Ctrl Pts',(-0.0141044995850598,-0.166650433334789,
1.1327348400487));
#37563=CARTESIAN_POINT('Ctrl Pts',(-0.0216594951399176,-0.166233867742642,
1.13241759971353));
#37564=CARTESIAN_POINT('Ctrl Pts',(-0.0291655735035569,-0.165315833865676,
1.13210018160962));
#37565=CARTESIAN_POINT('Ctrl Pts',(-0.0327092118793667,-0.164882427775424,
1.13195032772857));
#37566=CARTESIAN_POINT('Ctrl Pts',(-0.0362323925945039,-0.164338226995567,
1.13180083633464));
#37567=CARTESIAN_POINT('Ctrl Pts',(-0.0397271405986897,-0.163683459359474,
1.13165172827032));
#37568=CARTESIAN_POINT('Ctrl Pts',(-0.0499359232133337,-0.16177076624055,
1.13121615700369));
#37569=CARTESIAN_POINT('Ctrl Pts',(-0.0599087164806791,-0.158916175424461,
1.13078358684414));
#37570=CARTESIAN_POINT('Ctrl Pts',(-0.0695044280650932,-0.155097228857054,
1.13035212687658));
#37571=CARTESIAN_POINT('Ctrl Pts',(-0.0757996376989387,-0.152591831627178,
1.1300690701256));
#37572=CARTESIAN_POINT('Ctrl Pts',(-0.0819325841193579,-0.149670688079838,
1.12978649119439));
#37573=CARTESIAN_POINT('Ctrl Pts',(-0.0878818038415969,-0.146365274834167,
1.12950385616925));
#37574=CARTESIAN_POINT('Ctrl Pts',(-0.0910874459297812,-0.144584205666465,
1.12935156279727));
#37575=CARTESIAN_POINT('Ctrl Pts',(-0.09424019426452,-0.142690781721644,
1.129199221353));
#37576=CARTESIAN_POINT('Ctrl Pts',(-0.0973230172632952,-0.140698989172901,
1.12904742410559));
#37577=CARTESIAN_POINT('Ctrl Pts',(-0.107217543799977,-0.134306197813512,
1.12856022069066));
#37578=CARTESIAN_POINT('Ctrl Pts',(-0.116428399613608,-0.126885604548101,
1.12807698662012));
#37579=CARTESIAN_POINT('Ctrl Pts',(-0.124852487683086,-0.118613771136687,
1.12759508954235));
#37580=CARTESIAN_POINT('Ctrl Pts',(-0.129034307879819,-0.114507532011624,
1.12735586994778));
#37581=CARTESIAN_POINT('Ctrl Pts',(-0.133021908645802,-0.110190752518543,
1.12711697982177));
#37582=CARTESIAN_POINT('Ctrl Pts',(-0.136799920681752,-0.105681293454548,
1.12687809715289));
#37583=CARTESIAN_POINT('Ctrl Pts',(-0.139913092404994,-0.101965391993263,
1.12668125215535));
#37584=CARTESIAN_POINT('Ctrl Pts',(-0.142886395744951,-0.0981144149624532,
1.12648421657965));
#37585=CARTESIAN_POINT('Ctrl Pts',(-0.145693560119959,-0.0941626751454851,
1.12628802354802));
#37586=CARTESIAN_POINT('Ctrl Pts',(-0.152880478586678,-0.0840454080131806,
1.12578572901386));
#37587=CARTESIAN_POINT('Ctrl Pts',(-0.15900482121196,-0.0732463252276768,
1.12528759909576));
#37588=CARTESIAN_POINT('Ctrl Pts',(-0.163934147646496,-0.0619414999212126,
1.12479074962784));
#37589=CARTESIAN_POINT('Ctrl Pts',(-0.166135734382546,-0.0568924219632783,
1.1245688415816));
#37590=CARTESIAN_POINT('Ctrl Pts',(-0.168098373685913,-0.0517419572379162,
1.12434718895784));
#37591=CARTESIAN_POINT('Ctrl Pts',(-0.169806974463718,-0.0465039785200352,
1.12412553479695));
#37592=CARTESIAN_POINT('Ctrl Pts',(-0.171302024805205,-0.0419206715400791,
1.12393158420695));
#37593=CARTESIAN_POINT('Ctrl Pts',(-0.172603159720904,-0.037265702966286,
1.12373744627196));
#37594=CARTESIAN_POINT('Ctrl Pts',(-0.173693332107248,-0.0325769359939504,
1.12354412603317));
#37595=CARTESIAN_POINT('Ctrl Pts',(-0.174146803491923,-0.0306265823819912,
1.12346371196521));
#37596=CARTESIAN_POINT('Ctrl Pts',(-0.174564098410947,-0.0286695573112724,
1.12338340400172));
#37597=CARTESIAN_POINT('Ctrl Pts',(-0.174944665354966,-0.0267065873422436,
1.12330319031487));
#37598=CARTESIAN_POINT('Ctrl Pts',(-0.176644787249262,-0.0179373332737037,
1.1229448485109));
#37599=CARTESIAN_POINT('Ctrl Pts',(-0.177613299278372,-0.00904985393428815,
1.12258838819752));
#37600=CARTESIAN_POINT('Ctrl Pts',(-0.177892626630995,-0.00012009523392913,
1.12223275485995));
#37601=CARTESIAN_POINT('',(0.188128289424299,-0.051655738433239,1.1046));
#37602=CARTESIAN_POINT('Ctrl Pts',(0.188079991776263,-0.0516378774142054,
1.1046));
#37603=CARTESIAN_POINT('Ctrl Pts',(0.189767230432996,-0.0390669740826218,
1.10628778184834));
#37604=CARTESIAN_POINT('Ctrl Pts',(0.190280594088308,-0.0264116239428061,
1.10798825493552));
#37605=CARTESIAN_POINT('Ctrl Pts',(0.189578785198131,-0.013858618669063,
1.10971174069725));
#37606=CARTESIAN_POINT('Ctrl Pts',(0.189002564675101,-0.00355196771938053,
1.11112680950153));
#37607=CARTESIAN_POINT('Ctrl Pts',(0.187606197243972,0.00668612269204304,
1.11255739169934));
#37608=CARTESIAN_POINT('Ctrl Pts',(0.185342457317502,0.0167394104911895,
1.1140092000994));
#37609=CARTESIAN_POINT('Ctrl Pts',(0.184551132811226,0.0202536891903846,
1.1145167016688));
#37610=CARTESIAN_POINT('Ctrl Pts',(0.183655673454389,0.0237360512197014,
1.1150254747949));
#37611=CARTESIAN_POINT('Ctrl Pts',(0.18265534113529,0.0271808706561584,
1.11553563926267));
#37612=CARTESIAN_POINT('Ctrl Pts',(0.18094879298457,0.0330576679230306,
1.11640597026411));
#37613=CARTESIAN_POINT('Ctrl Pts',(0.178936945382248,0.038826456249319,
1.11728051290445));
#37614=CARTESIAN_POINT('Ctrl Pts',(0.176612263817241,0.0444636415640588,
1.1181607012295));
#37615=CARTESIAN_POINT('Ctrl Pts',(0.172529449099474,0.0543641731105064,
1.11970656708142));
#37616=CARTESIAN_POINT('Ctrl Pts',(0.167482382247398,0.0638604192469179,
1.12126984735358));
#37617=CARTESIAN_POINT('Ctrl Pts',(0.161567727140847,0.0728508334626257,
1.12285831080443));
#37618=CARTESIAN_POINT('Ctrl Pts',(0.159791310571961,0.0755510282307451,
1.12333539234888));
#37619=CARTESIAN_POINT('Ctrl Pts',(0.157935831204718,0.07820633305328,1.12381491808146));
#37620=CARTESIAN_POINT('Ctrl Pts',(0.156005857937656,0.080810555607592,
1.12429655968642));
#37621=CARTESIAN_POINT('Ctrl Pts',(0.149084780910453,0.0901495579668382,
1.12602377461955));
#37622=CARTESIAN_POINT('Ctrl Pts',(0.141258220296783,0.0987686403112959,
1.12776582990404));
#37623=CARTESIAN_POINT('Ctrl Pts',(0.132662596065602,0.106547632773669,
1.12953438681126));
#37624=CARTESIAN_POINT('Ctrl Pts',(0.125865807878512,0.11269868854969,1.13093283169111));
#37625=CARTESIAN_POINT('Ctrl Pts',(0.11858709408701,0.11832389399092,1.13234784666969));
#37626=CARTESIAN_POINT('Ctrl Pts',(0.110887722236713,0.123341541992538,
1.13378519708595));
#37627=CARTESIAN_POINT('Ctrl Pts',(0.108018415924993,0.125211456754541,
1.13432085099405));
#37628=CARTESIAN_POINT('Ctrl Pts',(0.105090557092059,0.126996521585399,
1.13485961189033));
#37629=CARTESIAN_POINT('Ctrl Pts',(0.102119703918859,0.128685646974318,
1.13539959124502));
#37630=CARTESIAN_POINT('Ctrl Pts',(0.0927768272952827,0.133997686711853,
1.13709774332326));
#37631=CARTESIAN_POINT('Ctrl Pts',(0.082979544177925,0.138384526176108,
1.13881348137989));
#37632=CARTESIAN_POINT('Ctrl Pts',(0.0728343136972591,0.141721417442936,
1.14055808556308));
#37633=CARTESIAN_POINT('Ctrl Pts',(0.0653892612002304,0.144170186912073,
1.14183835906254));
#37634=CARTESIAN_POINT('Ctrl Pts',(0.0577564921504827,0.146052612758731,
1.14313417790127));
#37635=CARTESIAN_POINT('Ctrl Pts',(0.0499806597877626,0.147301514408983,
1.14445));
#37636=CARTESIAN_POINT('',(0.156060797133591,0.117265290216009,1.1046));
#37637=CARTESIAN_POINT('Origin',(0.,0.,1.1046));
#37638=CARTESIAN_POINT('Ctrl Pts',(-0.177892626630995,-0.00012009523392913,
1.12223275485995));
#37639=CARTESIAN_POINT('Ctrl Pts',(-0.178130827469488,0.00749489839273535,
1.12192948288029));
#37640=CARTESIAN_POINT('Ctrl Pts',(-0.177867516731744,0.0151409018269471,
1.12162681218094));
#37641=CARTESIAN_POINT('Ctrl Pts',(-0.177119648653777,0.022772046405986,
1.12132408898598));
#37642=CARTESIAN_POINT('Ctrl Pts',(-0.176683933562239,0.0272180241883703,
1.12114771955869));
#37643=CARTESIAN_POINT('Ctrl Pts',(-0.176082727329522,0.0316616978614784,
1.1209712215835));
#37644=CARTESIAN_POINT('Ctrl Pts',(-0.175323410854016,0.0360699258071878,
1.12079542245302));
#37645=CARTESIAN_POINT('Ctrl Pts',(-0.173218074679692,0.0482924997380182,
1.12030798897732));
#37646=CARTESIAN_POINT('Ctrl Pts',(-0.169899117173377,0.060280772698104,
1.11982442300823));
#37647=CARTESIAN_POINT('Ctrl Pts',(-0.165450405286176,0.0718434015054524,
1.11934209182814));
#37648=CARTESIAN_POINT('Ctrl Pts',(-0.163468469691568,0.0769946421750163,
1.11912720955245));
#37649=CARTESIAN_POINT('Ctrl Pts',(-0.161261595477516,0.0820613755489734,
1.11891257235417));
#37650=CARTESIAN_POINT('Ctrl Pts',(-0.158833971908418,0.0870258740589896,
1.11869794744021));
#37651=CARTESIAN_POINT('Ctrl Pts',(-0.157259648823123,0.0902453701582717,
1.11855876237008));
#37652=CARTESIAN_POINT('Ctrl Pts',(-0.155591255289476,0.0934239508703652,
1.11841948892714));
#37653=CARTESIAN_POINT('Ctrl Pts',(-0.153833447558489,0.0965496328988143,
1.11828037128997));
#37654=CARTESIAN_POINT('Ctrl Pts',(-0.14771977559034,0.10742078465325,1.11779651882779));
#37655=CARTESIAN_POINT('Ctrl Pts',(-0.140558745189236,0.117602653899592,
1.11731683957354));
#37656=CARTESIAN_POINT('Ctrl Pts',(-0.132418289468816,0.126903043139938,
1.11683877992991));
#37657=CARTESIAN_POINT('Ctrl Pts',(-0.12909688936255,0.130697709540948,
1.11664372606491));
#37658=CARTESIAN_POINT('Ctrl Pts',(-0.125611892721837,0.134345412680643,
1.11644894182206));
#37659=CARTESIAN_POINT('Ctrl Pts',(-0.121965775424868,0.137831740927343,
1.11625425375315));
#37660=CARTESIAN_POINT('Ctrl Pts',(-0.117995359394073,0.141628155697328,
1.11604224942997));
#37661=CARTESIAN_POINT('Ctrl Pts',(-0.113833879872902,0.145233242900832,
1.11583035914965));
#37662=CARTESIAN_POINT('Ctrl Pts',(-0.109497995542763,0.148643456469952,
1.11561835894421));
#37663=CARTESIAN_POINT('Ctrl Pts',(-0.106528819965926,0.150978740824945,
1.11547318306212));
#37664=CARTESIAN_POINT('Ctrl Pts',(-0.103484861618328,0.153216986140016,
1.11532830099587));
#37665=CARTESIAN_POINT('Ctrl Pts',(-0.100375391374892,0.155356036404444,
1.11518378070706));
#37666=CARTESIAN_POINT('Ctrl Pts',(-0.0901590665073864,0.162383996377836,
1.11470895184398));
#37667=CARTESIAN_POINT('Ctrl Pts',(-0.0792284020877703,0.168351899996775,
1.11423755053895));
#37668=CARTESIAN_POINT('Ctrl Pts',(-0.0677866372531476,0.173236468334987,
1.11376713654095));
#37669=CARTESIAN_POINT('Ctrl Pts',(-0.0629527485252524,0.175300088779209,
1.11356839718953));
#37670=CARTESIAN_POINT('Ctrl Pts',(-0.0580272205709242,0.1771698553942,
1.11336983405985));
#37671=CARTESIAN_POINT('Ctrl Pts',(-0.053024031320765,0.178841703955505,
1.11317126314023));
#37672=CARTESIAN_POINT('Ctrl Pts',(-0.0477983789695303,0.180587890023723,
1.11296386291187));
#37673=CARTESIAN_POINT('Ctrl Pts',(-0.0424815416125505,0.182119285098682,
1.11275621043829));
#37674=CARTESIAN_POINT('Ctrl Pts',(-0.0371242414709178,0.183422331662166,
1.11254943891139));
#37675=CARTESIAN_POINT('Ctrl Pts',(-0.024630778610864,0.18646109436267,
1.11206723848886));
#37676=CARTESIAN_POINT('Ctrl Pts',(-0.0118919597510465,0.188273325293319,
1.11158873863955));
#37677=CARTESIAN_POINT('Ctrl Pts',(0.000886208579909016,0.188815541438236,
1.11111139386139));
#37678=CARTESIAN_POINT('Ctrl Pts',(0.00944159770367764,0.189178572350712,
1.1107917963872));
#37679=CARTESIAN_POINT('Ctrl Pts',(0.018015230692156,0.18897135417352,1.11047271669991));
#37680=CARTESIAN_POINT('Ctrl Pts',(0.0265466554166013,0.188167601942836,
1.11015339081081));
#37681=CARTESIAN_POINT('Ctrl Pts',(0.0302389326862781,0.187819749598396,
1.11001519118297));
#37682=CARTESIAN_POINT('Ctrl Pts',(0.0339178177085591,0.187360375525866,
1.1098771490423));
#37683=CARTESIAN_POINT('Ctrl Pts',(0.0375710017615334,0.186789297951633,
1.1097394835104));
#37684=CARTESIAN_POINT('Ctrl Pts',(0.0423078408099154,0.186048819915471,
1.10956098183688));
#37685=CARTESIAN_POINT('Ctrl Pts',(0.0470053189021468,0.185120233668386,
1.10938296950455));
#37686=CARTESIAN_POINT('Ctrl Pts',(0.0516529562716852,0.184000805096474,
1.10920531719144));
#37687=CARTESIAN_POINT('Ctrl Pts',(0.0618028867738203,0.181556095816553,
1.10881734401536));
#37688=CARTESIAN_POINT('Ctrl Pts',(0.0717155486830652,0.178202889727245,
1.10843108790673));
#37689=CARTESIAN_POINT('Ctrl Pts',(0.0813183120370126,0.174031280266035,
1.10804520187417));
#37690=CARTESIAN_POINT('Ctrl Pts',(0.0859478038432918,0.172020147521446,
1.10785916623421));
#37691=CARTESIAN_POINT('Ctrl Pts',(0.0905051909798001,0.169818426512715,
1.10767321660747));
#37692=CARTESIAN_POINT('Ctrl Pts',(0.0949816305437677,0.167434340091183,
1.10748720206377));
#37693=CARTESIAN_POINT('Ctrl Pts',(0.0983118022353031,0.165660739219842,
1.10734881968224));
#37694=CARTESIAN_POINT('Ctrl Pts',(0.101597049834463,0.16378593049508,1.10721040073536));
#37695=CARTESIAN_POINT('Ctrl Pts',(0.104821419449008,0.161821258958598,
1.10707241581092));
#37696=CARTESIAN_POINT('Ctrl Pts',(0.116000559886905,0.155009589811987,
1.10659401133715));
#37697=CARTESIAN_POINT('Ctrl Pts',(0.126488220095427,0.147101893720343,
1.10611923196118));
#37698=CARTESIAN_POINT('Ctrl Pts',(0.136144216947772,0.138260857674004,
1.10564559537577));
#37699=CARTESIAN_POINT('Ctrl Pts',(0.143255609150872,0.131749663048667,
1.1052967742678));
#37700=CARTESIAN_POINT('Ctrl Pts',(0.149915772834495,0.124730943289562,
1.10494857300279));
#37701=CARTESIAN_POINT('Ctrl Pts',(0.156057659382849,0.117255425406029,
1.1046));
#37702=CARTESIAN_POINT('',(-0.0999999999999999,-1.22464679914735E-17,1.2));
#37703=CARTESIAN_POINT('',(-0.15,-1.83697019872103E-17,1.15));
#37704=CARTESIAN_POINT('Origin',(0.,0.,1.2));
#37705=CARTESIAN_POINT('Ctrl Pts',(0.113509973994371,-0.159049193030953,
-0.0230074082272069));
#37706=CARTESIAN_POINT('Ctrl Pts',(0.166385127640631,-0.121313337847033,
-0.019303686544359));
#37707=CARTESIAN_POINT('Ctrl Pts',(0.230633516687349,0.0103782615975306,
-0.0118962431786632));
#37708=CARTESIAN_POINT('Ctrl Pts',(0.116188988078006,0.199753850566951,
-0.000785078130119459));
#37709=CARTESIAN_POINT('Ctrl Pts',(-0.104655428901899,0.205782953697956,
0.0103260869184242));
#37710=CARTESIAN_POINT('Ctrl Pts',(-0.229698075471667,0.0238333788527267,
0.0214372519669679));
#37711=CARTESIAN_POINT('Ctrl Pts',(-0.144613108848303,-0.180075271725216,
0.0325484170155115));
#37712=CARTESIAN_POINT('Ctrl Pts',(0.0727946961077783,-0.219149774367173,
0.0436595820640553));
#37713=CARTESIAN_POINT('Ctrl Pts',(0.22359411788162,-0.057762978583554,
0.0547707471125989));
#37714=CARTESIAN_POINT('Ctrl Pts',(0.169827668332871,0.156494259322429,
0.0658819121611427));
#37715=CARTESIAN_POINT('Ctrl Pts',(-0.0393188016825179,0.227560800163251,
0.0769930772096863));
#37716=CARTESIAN_POINT('Ctrl Pts',(-0.212490816724285,0.090434536960108,
0.0881042422582301));
#37717=CARTESIAN_POINT('Ctrl Pts',(-0.19125222930514,-0.129434912039326,
0.0992154073067737));
#37718=CARTESIAN_POINT('Ctrl Pts',(0.00496630258143332,-0.230880650358359,
0.110326572355317));
#37719=CARTESIAN_POINT('Ctrl Pts',(0.196640931676781,-0.121090966106477,
0.121437737403861));
#37720=CARTESIAN_POINT('Ctrl Pts',(0.208405785032279,0.0994871990457256,
0.132548902452405));
#37721=CARTESIAN_POINT('Ctrl Pts',(0.0294968904732024,0.229042728261432,
0.143660067500948));
#37722=CARTESIAN_POINT('Ctrl Pts',(-0.176399147035948,0.149043619583305,
0.154771232549492));
#37723=CARTESIAN_POINT('Ctrl Pts',(-0.220904863824581,-0.0673178902258552,
0.165882397598036));
#37724=CARTESIAN_POINT('Ctrl Pts',(-0.0633012670336293,-0.222089176195486,
0.17699356264658));
#37725=CARTESIAN_POINT('Ctrl Pts',(0.152217643594786,-0.173667627565877,
0.188104727695123));
#37726=CARTESIAN_POINT('Ctrl Pts',(0.228470258285089,0.0336451535954383,
0.199215892743667));
#37727=CARTESIAN_POINT('Ctrl Pts',(0.0956918672404541,0.210175453516431,
0.210327057792211));
#37728=CARTESIAN_POINT('Ctrl Pts',(-0.124636506047609,0.194412953698174,
0.221438222840754));
#37729=CARTESIAN_POINT('Ctrl Pts',(-0.230932995110325,0.000779007092406014,
0.232549387889298));
#37730=CARTESIAN_POINT('Ctrl Pts',(-0.12594528285163,-0.193567664513544,
0.243660552937842));
#37731=CARTESIAN_POINT('Ctrl Pts',(0.0942717341349318,-0.21081625941051,
0.254771717986386));
#37732=CARTESIAN_POINT('Ctrl Pts',(0.228238070382781,-0.0351857683462,0.265882883034929));
#37733=CARTESIAN_POINT('Ctrl Pts',(0.153385834111148,0.172636731182735,
0.276994048083473));
#37734=CARTESIAN_POINT('Ctrl Pts',(-0.0618014955343493,0.222511191222357,
0.288105213132016));
#37735=CARTESIAN_POINT('Ctrl Pts',(-0.220445672440028,0.068806689849701,
0.299216378180561));
#37736=CARTESIAN_POINT('Ctrl Pts',(-0.177400663329184,-0.147850125855229,
0.310327543229104));
#37737=CARTESIAN_POINT('Ctrl Pts',(0.0279509811935462,-0.229236554058792,
0.321438708277648));
#37738=CARTESIAN_POINT('Ctrl Pts',(0.207729836817097,-0.100890881459812,
0.332549873326191));
#37739=CARTESIAN_POINT('Ctrl Pts',(0.197453422882556,0.11976143309821,0.343661038374735));
#37740=CARTESIAN_POINT('Ctrl Pts',(0.00652379087403971,0.230842143506323,
0.354772203423278));
#37741=CARTESIAN_POINT('Ctrl Pts',(-0.190374559216213,0.130721774273047,
0.365883368471823));
#37742=CARTESIAN_POINT('Ctrl Pts',(-0.213096254074054,-0.0889979863001003,
0.376994533520366));
#37743=CARTESIAN_POINT('Ctrl Pts',(-0.0408528604769679,-0.227292100295502,
0.38810569856891));
#37744=CARTESIAN_POINT('Ctrl Pts',(0.16876745272456,-0.15763312458598,0.399216863617453));
#37745=CARTESIAN_POINT('Ctrl Pts',(0.223979789625721,0.0562468568463683,
0.410328028665997));
#37746=CARTESIAN_POINT('Ctrl Pts',(0.0742695215461042,0.218665711155622,
0.421439193714541));
#37747=CARTESIAN_POINT('Ctrl Pts',(-0.143391090854028,0.181023893808443,
0.432550358763085));
#37748=CARTESIAN_POINT('Ctrl Pts',(-0.229860956455329,-0.0222395090620434,
0.443661523811628));
#37749=CARTESIAN_POINT('Ctrl Pts',(-0.106027445761331,-0.205155638019547,
0.454772688860172));
#37750=CARTESIAN_POINT('Ctrl Pts',(0.114812229735204,-0.200371672072451,
0.465883853908716));
#37751=CARTESIAN_POINT('Ctrl Pts',(0.230608404475241,-0.0122645363248325,
0.476995018957259));
#37752=CARTESIAN_POINT('Ctrl Pts',(0.135417351061808,0.187063615108022,
0.488106184005803));
#37753=CARTESIAN_POINT('Ctrl Pts',(-0.083669150175529,0.21524434574405,
0.499217349054346));
#37754=CARTESIAN_POINT('Ctrl Pts',(-0.226205440167697,0.0464946653328952,
0.510328514102891));
#37755=CARTESIAN_POINT('Ctrl Pts',(-0.161782842764492,-0.164793709991974,
0.521439679151433));
#37756=CARTESIAN_POINT('Ctrl Pts',(0.0506574022840452,-0.225309748257175,
0.532550844199978));
#37757=CARTESIAN_POINT('Ctrl Pts',(0.21675039941815,-0.0796863816342033,
0.543662009248521));
#37758=CARTESIAN_POINT('Ctrl Pts',(0.184535073495005,0.138843299139974,
0.554773174297065));
#37759=CARTESIAN_POINT('Ctrl Pts',(-0.01651427104253,0.230343078727826,
0.565884339345609));
#37760=CARTESIAN_POINT('Ctrl Pts',(-0.2024544512798,0.11109838082922,0.576995504394152));
#37761=CARTESIAN_POINT('Ctrl Pts',(-0.203165894515671,-0.109791959503082,
0.588106669442697));
#37762=CARTESIAN_POINT('Ctrl Pts',(-0.0179976902307884,-0.230231922661119,
0.599217834491239));
#37763=CARTESIAN_POINT('Ctrl Pts',(0.183636881720094,-0.140029106752845,
0.610328999539785));
#37764=CARTESIAN_POINT('Ctrl Pts',(0.217259204728728,0.0782885242326115,
0.621440164588326));
#37765=CARTESIAN_POINT('Ctrl Pts',(0.0521076907609949,0.224978762618687,
0.632551329636872));
#37766=CARTESIAN_POINT('Ctrl Pts',(-0.160717962682088,0.16583242004264,
0.643662494685413));
#37767=CARTESIAN_POINT('Ctrl Pts',(-0.226500243885858,-0.0450365916286509,
0.65477365973396));
#37768=CARTESIAN_POINT('Ctrl Pts',(-0.0850539171717745,-0.214700922773088,
0.665884824782501));
#37769=CARTESIAN_POINT('Ctrl Pts',(0.134209565723166,-0.187932029027199,
0.676995989831046));
#37770=CARTESIAN_POINT('Ctrl Pts',(0.230682622449346,0.0107788109627418,
0.68810715487959));
#37771=CARTESIAN_POINT('Ctrl Pts',(0.116100547839306,0.199627948587589,
0.699218319928133));
#37772=CARTESIAN_POINT('Ctrl Pts',(-0.104703729866326,0.205834360634882,
0.710329484976677));
#37773=CARTESIAN_POINT('Ctrl Pts',(-0.229712931099768,0.0237197038645086,
0.721440650025221));
#37774=CARTESIAN_POINT('Ctrl Pts',(-0.144554186745893,-0.180096480143545,
0.732551815073763));
#37775=CARTESIAN_POINT('Ctrl Pts',(0.072859438989827,-0.219139583863915,
0.743662980122308));
#37776=CARTESIAN_POINT('Ctrl Pts',(0.223612826941383,-0.0576884623911715,
0.75477414517085));
#37777=CARTESIAN_POINT('Ctrl Pts',(0.16977934979946,0.156542733614398,0.765885310219396));
#37778=CARTESIAN_POINT('Ctrl Pts',(-0.0393879040694563,0.227550539615811,
0.776996475267938));
#37779=CARTESIAN_POINT('Ctrl Pts',(-0.212518549811472,0.0903688057410859,
0.788107640316484));
#37780=CARTESIAN_POINT('Ctrl Pts',(-0.191212657747833,-0.129492758803799,
0.799218805365025));
#37781=CARTESIAN_POINT('Ctrl Pts',(0.00503667898133586,-0.230879377455661,
0.81032997041357));
#37782=CARTESIAN_POINT('Ctrl Pts',(0.196677879493939,-0.121030850518371,
0.821441135462113));
#37783=CARTESIAN_POINT('Ctrl Pts',(0.208375418707704,0.0995506903268707,
0.832552300510658));
#37784=CARTESIAN_POINT('Ctrl Pts',(0.0294270353677539,0.229051751091564,
0.8436634655592));
#37785=CARTESIAN_POINT('Ctrl Pts',(-0.176444601777748,0.14898978999011,
0.854774630607746));
#37786=CARTESIAN_POINT('Ctrl Pts',(-0.22088431932234,-0.0673852547682493,
0.865885795656288));
#37787=CARTESIAN_POINT('Ctrl Pts',(-0.0632335256349382,-0.22210847899434,
0.876996960704833));
#37788=CARTESIAN_POINT('Ctrl Pts',(0.152270606837662,-0.173621188252162,
0.888108125753376));
#37789=CARTESIAN_POINT('Ctrl Pts',(0.228459985995541,0.0337148347205355,
0.899219290801919));
#37790=CARTESIAN_POINT('Ctrl Pts',(0.0956277562497704,0.210204633917866,
0.910330455850463));
#37791=CARTESIAN_POINT('Ctrl Pts',(-0.12469579560031,0.194374924182257,
0.921441620899007));
#37792=CARTESIAN_POINT('Ctrl Pts',(-0.230933226540692,0.000708579792413808,
0.932552785947551));
#37793=CARTESIAN_POINT('Ctrl Pts',(-0.125886228368054,-0.193606087509586,
0.943663950996094));
#37794=CARTESIAN_POINT('Ctrl Pts',(0.0943360139257667,-0.210787462610152,
0.954775116044639));
#37795=CARTESIAN_POINT('Ctrl Pts',(0.228248823506631,-0.0351162152961091,
0.965886281093181));
#37796=CARTESIAN_POINT('Ctrl Pts',(0.153333110744206,0.172683627576032,
0.976997446141726));
#37797=CARTESIAN_POINT('Ctrl Pts',(-0.0618692454411617,0.222492101746939,
0.988108611190268));
#37798=CARTESIAN_POINT('Ctrl Pts',(-0.220466868021367,0.0687398848825245,
0.999219776238814));
#37799=CARTESIAN_POINT('Ctrl Pts',(-0.17735514221838,-0.147905058047522,
1.01033094128735));
#37800=CARTESIAN_POINT('Ctrl Pts',(0.0280201048116106,-0.229226437530741,
1.0214421063359));
#37801=CARTESIAN_POINT('Ctrl Pts',(0.207762111854432,-0.10083052618152,
1.03255327138444));
#37802=CARTESIAN_POINT('Ctrl Pts',(0.197414006873683,0.119827380577986,
1.04366443643299));
#37803=CARTESIAN_POINT('Ctrl Pts',(0.00645886152005097,0.230833217918201,
1.05477560148153));
#37804=CARTESIAN_POINT('Ctrl Pts',(-0.190424854748374,0.130684465150768,
1.06588676653008));
#37805=CARTESIAN_POINT('Ctrl Pts',(-0.213049227679005,-0.0891025387309722,
1.07699793157862));
#37806=CARTESIAN_POINT('Ctrl Pts',(-0.0408214485225542,-0.227228942196666,
1.08810909662716));
#37807=CARTESIAN_POINT('Ctrl Pts',(0.168888461736298,-0.15772814986318,
1.09922026167571));
#37808=CARTESIAN_POINT('Ctrl Pts',(0.223817187934597,0.0566161966084782,
1.11033142672425));
#37809=CARTESIAN_POINT('Ctrl Pts',(0.124300218570944,0.164165746435707,
1.11773887008995));
#37810=CARTESIAN_POINT('Ctrl Pts',(0.0627850911123727,0.1850383536838,1.12144259177279));
#37811=CARTESIAN_POINT('Ctrl Pts',(0.105793541951254,-0.14823699524473,
-0.0153382721514713));
#37812=CARTESIAN_POINT('Ctrl Pts',(0.155074231467859,-0.113066431478549,
-0.0116345504686234));
#37813=CARTESIAN_POINT('Ctrl Pts',(0.214955001436596,0.00967274517879857,
-0.00422710710292769));
#37814=CARTESIAN_POINT('Ctrl Pts',(0.108290436090784,0.186174541551099,
0.00688405794561606));
#37815=CARTESIAN_POINT('Ctrl Pts',(-0.0975409307071879,0.191793784975909,
0.0179952229941597));
#37816=CARTESIAN_POINT('Ctrl Pts',(-0.214083151712633,0.022213180716797,
0.0291063880427034));
#37817=CARTESIAN_POINT('Ctrl Pts',(-0.134782279118508,-0.167833716661673,
0.0402175530912472));
#37818=CARTESIAN_POINT('Ctrl Pts',(0.0678460972679723,-0.204251926348524,
0.0513287181397908));
#37819=CARTESIAN_POINT('Ctrl Pts',(0.208394142450739,-0.0538362390807298,
0.0624398831883346));
#37820=CARTESIAN_POINT('Ctrl Pts',(0.158282747515632,0.145855746470163,
0.0735510482368781));
#37821=CARTESIAN_POINT('Ctrl Pts',(-0.0366459012269607,0.212091168831785,
0.084662213285422));
#37822=CARTESIAN_POINT('Ctrl Pts',(-0.198045646054783,0.0842867780077688,
0.0957733783339656));
#37823=CARTESIAN_POINT('Ctrl Pts',(-0.178250862301028,-0.120635899339281,
0.106884543382509));
#37824=CARTESIAN_POINT('Ctrl Pts',(0.00462869228141735,-0.215185334908375,
0.117995708431053));
#37825=CARTESIAN_POINT('Ctrl Pts',(0.183273239545565,-0.112859176615955,
0.129106873479597));
#37826=CARTESIAN_POINT('Ctrl Pts',(0.194238315681312,0.0927240382098824,
0.14021803852814));
#37827=CARTESIAN_POINT('Ctrl Pts',(0.0274916856192995,0.213472355144377,
0.151329203576684));
#37828=CARTESIAN_POINT('Ctrl Pts',(-0.164407495706399,0.138911602796551,
0.162440368625228));
#37829=CARTESIAN_POINT('Ctrl Pts',(-0.20588770445336,-0.062741605808422,
0.173551533673771));
#37830=CARTESIAN_POINT('Ctrl Pts',(-0.0589980335104445,-0.206991507018771,
0.184662698722315));
#37831=CARTESIAN_POINT('Ctrl Pts',(0.141869855984326,-0.161861665507704,
0.195773863770859));
#37832=CARTESIAN_POINT('Ctrl Pts',(0.21293880179812,0.0313579489369987,
0.206885028819403));
#37833=CARTESIAN_POINT('Ctrl Pts',(0.0891867138635642,0.195887681727571,
0.217996193867946));
#37834=CARTESIAN_POINT('Ctrl Pts',(-0.116163690001897,0.18119671998123,
0.22910735891649));
#37835=CARTESIAN_POINT('Ctrl Pts',(-0.21523412125303,0.00072605002547781,
0.240218523965033));
#37836=CARTESIAN_POINT('Ctrl Pts',(-0.11738349588193,-0.180408893734178,
0.251329689013577));
#37837=CARTESIAN_POINT('Ctrl Pts',(0.0878631217069615,-0.196484925501419,
0.262440854062121));
#37838=CARTESIAN_POINT('Ctrl Pts',(0.212722398078527,-0.0327938323711113,
0.273552019110664));
#37839=CARTESIAN_POINT('Ctrl Pts',(0.142958632662274,0.160900849678758,
0.284663184159209));
#37840=CARTESIAN_POINT('Ctrl Pts',(-0.057600216794938,0.207384833374845,
0.295774349207752));
#37841=CARTESIAN_POINT('Ctrl Pts',(-0.205459728996263,0.0641291965189069,
0.306885514256296));
#37842=CARTESIAN_POINT('Ctrl Pts',(-0.165340928710165,-0.137799243024573,
0.317996679304839));
#37843=CARTESIAN_POINT('Ctrl Pts',(0.0260508675794864,-0.213653004623031,
0.329107844353384));
#37844=CARTESIAN_POINT('Ctrl Pts',(0.193608318568785,-0.0940322979965331,
0.340219009401926));
#37845=CARTESIAN_POINT('Ctrl Pts',(0.184030497427301,0.111620025542831,
0.351330174450471));
#37846=CARTESIAN_POINT('Ctrl Pts',(0.00608030219043116,0.215149445760286,
0.362441339499014));
#37847=CARTESIAN_POINT('Ctrl Pts',(-0.177432856410404,0.121835280406139,
0.373552504547559));
#37848=CARTESIAN_POINT('Ctrl Pts',(-0.198609925645444,-0.0829478843655077,
0.384663669596101));
#37849=CARTESIAN_POINT('Ctrl Pts',(-0.0380756743800589,-0.211840735237885,
0.395774834644646));
#37850=CARTESIAN_POINT('Ctrl Pts',(0.157294605588646,-0.14691719143219,
0.406885999693188));
#37851=CARTESIAN_POINT('Ctrl Pts',(0.208753596148093,0.0524231836199493,
0.417997164741733));
#37852=CARTESIAN_POINT('Ctrl Pts',(0.0692206637610257,0.203800769856489,
0.429108329790276));
#37853=CARTESIAN_POINT('Ctrl Pts',(-0.133643334165982,0.168717851215016,
0.44021949483882));
#37854=CARTESIAN_POINT('Ctrl Pts',(-0.21423496001257,-0.0207276625316418,
0.451330659887364));
#37855=CARTESIAN_POINT('Ctrl Pts',(-0.0988196775702872,-0.191209114350017,
0.462441824935908));
#37856=CARTESIAN_POINT('Ctrl Pts',(0.107007270071357,-0.186750363419964,
0.473552989984451));
#37857=CARTESIAN_POINT('Ctrl Pts',(0.21493159635798,-0.011430790551128,
0.484664155032995));
#37858=CARTESIAN_POINT('Ctrl Pts',(0.126211650891535,0.174346990983058,
0.495775320081538));
#37859=CARTESIAN_POINT('Ctrl Pts',(-0.0779813036479037,0.200611989589323,
0.506886485130082));
#37860=CARTESIAN_POINT('Ctrl Pts',(-0.21082794649543,0.0433339481484583,
0.517997650178626));
#37861=CARTESIAN_POINT('Ctrl Pts',(-0.150784810891129,-0.153590998727594,
0.529108815227169));
#37862=CARTESIAN_POINT('Ctrl Pts',(0.0472137013611209,-0.209993143910453,
0.540219980275713));
#37863=CARTESIAN_POINT('Ctrl Pts',(0.202015661416081,-0.0742692845544967,
0.551331145324257));
#37864=CARTESIAN_POINT('Ctrl Pts',(0.171990340163759,0.129404702294652,
0.562442310372801));
#37865=CARTESIAN_POINT('Ctrl Pts',(-0.0153916274037652,0.214684307510999,
0.573553475421344));
#37866=CARTESIAN_POINT('Ctrl Pts',(-0.188691554856225,0.103545889399597,
0.584664640469888));
#37867=CARTESIAN_POINT('Ctrl Pts',(-0.189354634030427,-0.102328278871562,
0.595775805518432));
#37868=CARTESIAN_POINT('Ctrl Pts',(-0.0167742034418123,-0.21458070785722,
0.606886970566975));
#37869=CARTESIAN_POINT('Ctrl Pts',(0.171153207655705,-0.130509898455162,
0.61799813561552));
#37870=CARTESIAN_POINT('Ctrl Pts',(0.202489878034016,0.0729664537947597,
0.629109300664062));
#37871=CARTESIAN_POINT('Ctrl Pts',(0.0485653989206222,0.209684658745684,
0.640220465712607));
#37872=CARTESIAN_POINT('Ctrl Pts',(-0.149792321581985,0.154559097049293,
0.65133163076115));
#37873=CARTESIAN_POINT('Ctrl Pts',(-0.211102709394471,-0.041974994603061,
0.662442795809694));
#37874=CARTESIAN_POINT('Ctrl Pts',(-0.079271933890819,-0.20010550862688,
0.673553960858237));
#37875=CARTESIAN_POINT('Ctrl Pts',(0.125085971055702,-0.17515636994031,
0.684665125906781));
#37876=CARTESIAN_POINT('Ctrl Pts',(0.215000768978506,0.0100460651134341,
0.695776290955325));
#37877=CARTESIAN_POINT('Ctrl Pts',(0.108208008038219,0.186057198414926,
0.706887456003868));
#37878=CARTESIAN_POINT('Ctrl Pts',(-0.0975859481618359,0.191841697258389,
0.717998621052413));
#37879=CARTESIAN_POINT('Ctrl Pts',(-0.214096997451993,0.0221072333783236,
0.729109786100956));
#37880=CARTESIAN_POINT('Ctrl Pts',(-0.134727362553083,-0.167853483327237,
0.7402209511495));
#37881=CARTESIAN_POINT('Ctrl Pts',(0.0679064389152043,-0.204242428597833,
0.751332116198043));
#37882=CARTESIAN_POINT('Ctrl Pts',(0.208411579664662,-0.0537667885148679,
0.762443281246587));
#37883=CARTESIAN_POINT('Ctrl Pts',(0.158237713686343,0.14590092546951,0.773554446295131));
#37884=CARTESIAN_POINT('Ctrl Pts',(-0.0367103060190181,0.21208160579853,
0.784665611343674));
#37885=CARTESIAN_POINT('Ctrl Pts',(-0.198071493840836,0.0842255152109201,
0.795776776392219));
#37886=CARTESIAN_POINT('Ctrl Pts',(-0.178213980826558,-0.120689813668469,
0.80688794144076));
#37887=CARTESIAN_POINT('Ctrl Pts',(0.00469428447876819,-0.215184148537872,
0.817999106489307));
#37888=CARTESIAN_POINT('Ctrl Pts',(0.183307675642296,-0.112803147698245,
0.829110271537848));
#37889=CARTESIAN_POINT('Ctrl Pts',(0.194210013665906,0.0927832133403047,
0.840221436586394));
#37890=CARTESIAN_POINT('Ctrl Pts',(0.0274265792786954,0.213480764600607,
0.851332601634936));
#37891=CARTESIAN_POINT('Ctrl Pts',(-0.164449860425235,0.138861432550488,
0.86244376668348));
#37892=CARTESIAN_POINT('Ctrl Pts',(-0.205868556570727,-0.0628043908949741,
0.873554931732024));
#37893=CARTESIAN_POINT('Ctrl Pts',(-0.0589348971863656,-0.207009497609277,
0.884666096780567));
#37894=CARTESIAN_POINT('Ctrl Pts',(0.141919218774748,-0.161818383148359,
0.895777261829112));
#37895=CARTESIAN_POINT('Ctrl Pts',(0.212929227820989,0.0314228931244718,
0.906888426877654));
#37896=CARTESIAN_POINT('Ctrl Pts',(0.0891269611515884,0.195914878439144,
0.9179995919262));
#37897=CARTESIAN_POINT('Ctrl Pts',(-0.116218949038264,0.181161275719849,
0.929110756974741));
#37898=CARTESIAN_POINT('Ctrl Pts',(-0.215234336950711,0.000660410388236847,
0.940221922023287));
#37899=CARTESIAN_POINT('Ctrl Pts',(-0.117328455934639,-0.180444704726821,
0.951333087071829));
#37900=CARTESIAN_POINT('Ctrl Pts',(0.0879230317440182,-0.196458086313641,
0.962444252120374));
#37901=CARTESIAN_POINT('Ctrl Pts',(0.212732420202743,-0.0327290075520782,
0.973555417168917));
#37902=CARTESIAN_POINT('Ctrl Pts',(0.142909493440969,0.160944558045319,
0.98466658221746));
#37903=CARTESIAN_POINT('Ctrl Pts',(-0.0576633610487541,0.207367041606005,
0.995777747266004));
#37904=CARTESIAN_POINT('Ctrl Pts',(-0.205479483697499,0.0640669329675303,
1.00688891231455));
#37905=CARTESIAN_POINT('Ctrl Pts',(-0.165298502134104,-0.137850440914814,
1.01800007736309));
#37906=CARTESIAN_POINT('Ctrl Pts',(0.026115292159373,-0.213643575818697,
1.02911124241164));
#37907=CARTESIAN_POINT('Ctrl Pts',(0.193638399542254,-0.0939760456828254,
1.04022240746018));
#37908=CARTESIAN_POINT('Ctrl Pts',(0.183993760927049,0.111681489898982,
1.05133357250872));
#37909=CARTESIAN_POINT('Ctrl Pts',(0.00601978674766102,0.215141126935532,
1.06244473755726));
#37910=CARTESIAN_POINT('Ctrl Pts',(-0.177479732841649,0.121800507565884,
1.07355590260581));
#37911=CARTESIAN_POINT('Ctrl Pts',(-0.198566096114678,-0.0830453293000129,
1.08466706765435));
#37912=CARTESIAN_POINT('Ctrl Pts',(-0.0380463978169507,-0.211781870639967,
1.0957782327029));
#37913=CARTESIAN_POINT('Ctrl Pts',(0.157407388382168,-0.147005756870945,
1.10688939775144));
#37914=CARTESIAN_POINT('Ctrl Pts',(0.208602048154327,0.0527674155869038,
1.11800056279999));
#37915=CARTESIAN_POINT('Ctrl Pts',(0.115850263419028,0.153005724266717,
1.12540800616568));
#37916=CARTESIAN_POINT('Ctrl Pts',(0.0585169473375027,0.172459407258861,
1.12911172784853));
#37917=CARTESIAN_POINT('Ctrl Pts',(0.0980771099081375,-0.137424797458507,
-0.00766913607573581));
#37918=CARTESIAN_POINT('Ctrl Pts',(0.143763335295088,-0.104819525110066,
-0.00396541439288791));
#37919=CARTESIAN_POINT('Ctrl Pts',(0.199276486185844,0.0089672287600667,
0.00344202897280782));
#37920=CARTESIAN_POINT('Ctrl Pts',(0.100391884103562,0.172595232535247,
0.0145531940213516));
#37921=CARTESIAN_POINT('Ctrl Pts',(-0.0904264325124765,0.177804616253862,
0.0256643590698952));
#37922=CARTESIAN_POINT('Ctrl Pts',(-0.198468227953599,0.020592982580867,
0.036775524118439));
#37923=CARTESIAN_POINT('Ctrl Pts',(-0.124951449388714,-0.155592161598129,
0.0478866891669827));
#37924=CARTESIAN_POINT('Ctrl Pts',(0.0628974984281669,-0.189354078329874,
0.0589978542155263));
#37925=CARTESIAN_POINT('Ctrl Pts',(0.193194167019859,-0.0499094995779056,
0.07010901926407));
#37926=CARTESIAN_POINT('Ctrl Pts',(0.146737826698393,0.135217233617898,
0.0812201843126137));
#37927=CARTESIAN_POINT('Ctrl Pts',(-0.0339730007714042,0.196621537500318,
0.0923313493611574));
#37928=CARTESIAN_POINT('Ctrl Pts',(-0.18360047538528,0.07813901905543,0.103442514409701));
#37929=CARTESIAN_POINT('Ctrl Pts',(-0.165249495296916,-0.111836886639236,
0.114553679458245));
#37930=CARTESIAN_POINT('Ctrl Pts',(0.00429108198140191,-0.199490019458391,
0.125664844506789));
#37931=CARTESIAN_POINT('Ctrl Pts',(0.169905547414348,-0.104627387125433,
0.136776009555332));
#37932=CARTESIAN_POINT('Ctrl Pts',(0.180070846330345,0.0859608773740392,
0.147887174603876));
#37933=CARTESIAN_POINT('Ctrl Pts',(0.0254864807653961,0.197901982027321,
0.15899833965242));
#37934=CARTESIAN_POINT('Ctrl Pts',(-0.152415844376849,0.128779586009797,
0.170109504700963));
#37935=CARTESIAN_POINT('Ctrl Pts',(-0.190870545082139,-0.0581653213909888,
0.181220669749507));
#37936=CARTESIAN_POINT('Ctrl Pts',(-0.0546947999872595,-0.191893837842057,
0.192331834798051));
#37937=CARTESIAN_POINT('Ctrl Pts',(0.131522068373867,-0.150055703449532,
0.203442999846594));
#37938=CARTESIAN_POINT('Ctrl Pts',(0.197407345311151,0.0290707442785592,
0.214554164895138));
#37939=CARTESIAN_POINT('Ctrl Pts',(0.0826815604866742,0.181599909938712,
0.225665329943681));
#37940=CARTESIAN_POINT('Ctrl Pts',(-0.107690873956185,0.167980486264285,
0.236776494992226));
#37941=CARTESIAN_POINT('Ctrl Pts',(-0.199535247395734,0.000673092958549589,
0.247887660040769));
#37942=CARTESIAN_POINT('Ctrl Pts',(-0.10882170891223,-0.167250122954812,
0.258998825089313));
#37943=CARTESIAN_POINT('Ctrl Pts',(0.0814545092789914,-0.182153591592328,
0.270109990137857));
#37944=CARTESIAN_POINT('Ctrl Pts',(0.197206725774273,-0.0304018963960226,
0.2812211551864));
#37945=CARTESIAN_POINT('Ctrl Pts',(0.1325314312134,0.149164968174781,0.292332320234944));
#37946=CARTESIAN_POINT('Ctrl Pts',(-0.0533989380555266,0.192258475527334,
0.303443485283487));
#37947=CARTESIAN_POINT('Ctrl Pts',(-0.190473785552499,0.0594517031881129,
0.314554650332031));
#37948=CARTESIAN_POINT('Ctrl Pts',(-0.153281194091147,-0.127748360193918,
0.325665815380575));
#37949=CARTESIAN_POINT('Ctrl Pts',(0.0241507539654265,-0.198069455187271,
0.336776980429119));
#37950=CARTESIAN_POINT('Ctrl Pts',(0.179486800320472,-0.0871737145332536,
0.347888145477662));
#37951=CARTESIAN_POINT('Ctrl Pts',(0.170607571972046,0.103478617987453,
0.358999310526206));
#37952=CARTESIAN_POINT('Ctrl Pts',(0.00563681350682242,0.199456748014249,
0.37011047557475));
#37953=CARTESIAN_POINT('Ctrl Pts',(-0.164491153604594,0.11294878653923,
0.381221640623293));
#37954=CARTESIAN_POINT('Ctrl Pts',(-0.184123597216834,-0.0768977824309152,
0.392332805671837));
#37955=CARTESIAN_POINT('Ctrl Pts',(-0.0352984882831497,-0.196389370180267,
0.403443970720381));
#37956=CARTESIAN_POINT('Ctrl Pts',(0.145821758452731,-0.136201258278399,
0.414555135768924));
#37957=CARTESIAN_POINT('Ctrl Pts',(0.193527402670466,0.0485995103935303,
0.425666300817468));
#37958=CARTESIAN_POINT('Ctrl Pts',(0.0641718059759468,0.188935828557357,
0.436777465866012));
#37959=CARTESIAN_POINT('Ctrl Pts',(-0.123895577477937,0.156411808621589,
0.447888630914555));
#37960=CARTESIAN_POINT('Ctrl Pts',(-0.198608963569812,-0.01921581600124,
0.458999795963099));
#37961=CARTESIAN_POINT('Ctrl Pts',(-0.0916119093792434,-0.177262590680487,
0.470110961011643));
#37962=CARTESIAN_POINT('Ctrl Pts',(0.0992023104075105,-0.173129054767478,
0.481222126060186));
#37963=CARTESIAN_POINT('Ctrl Pts',(0.199254788240719,-0.0105970447774237,
0.49233329110873));
#37964=CARTESIAN_POINT('Ctrl Pts',(0.117005950721263,0.161630366858093,
0.503444456157274));
#37965=CARTESIAN_POINT('Ctrl Pts',(-0.0722934571202785,0.185979633434597,
0.514555621205818));
#37966=CARTESIAN_POINT('Ctrl Pts',(-0.195450452823164,0.0401732309640217,
0.525666786254361));
#37967=CARTESIAN_POINT('Ctrl Pts',(-0.139786779017765,-0.142388287463214,
0.536777951302905));
#37968=CARTESIAN_POINT('Ctrl Pts',(0.0437700004381964,-0.19467653956373,
0.547889116351449));
#37969=CARTESIAN_POINT('Ctrl Pts',(0.187280923414012,-0.0688521874747905,
0.559000281399993));
#37970=CARTESIAN_POINT('Ctrl Pts',(0.159445606832513,0.119966105449332,
0.570111446448536));
#37971=CARTESIAN_POINT('Ctrl Pts',(-0.0142689837650004,0.199025536294172,
0.581222611497081));
#37972=CARTESIAN_POINT('Ctrl Pts',(-0.174928658432651,0.0959933979699734,
0.592333776545623));
#37973=CARTESIAN_POINT('Ctrl Pts',(-0.175543373545183,-0.0948645982400418,
0.603444941594168));
#37974=CARTESIAN_POINT('Ctrl Pts',(-0.0155507166528361,-0.198929493053321,
0.61455610664271));
#37975=CARTESIAN_POINT('Ctrl Pts',(0.158669533591315,-0.120990690157479,
0.625667271691256));
#37976=CARTESIAN_POINT('Ctrl Pts',(0.187720551339304,0.0676443833569079,
0.636778436739797));
#37977=CARTESIAN_POINT('Ctrl Pts',(0.0450231070802491,0.194390554872681,
0.647889601788343));
#37978=CARTESIAN_POINT('Ctrl Pts',(-0.138866680481881,0.143285774055946,
0.659000766836885));
#37979=CARTESIAN_POINT('Ctrl Pts',(-0.195705174903083,-0.038913397577471,
0.67011193188543));
#37980=CARTESIAN_POINT('Ctrl Pts',(-0.0734899506098636,-0.185510094480672,
0.681223096933973));
#37981=CARTESIAN_POINT('Ctrl Pts',(0.115962376388238,-0.162380710853421,
0.692334261982516));
#37982=CARTESIAN_POINT('Ctrl Pts',(0.199318915507666,0.00931331926412601,
0.703445427031061));
#37983=CARTESIAN_POINT('Ctrl Pts',(0.100315468237132,0.172486448242263,
0.714556592079604));
#37984=CARTESIAN_POINT('Ctrl Pts',(-0.0904681664573454,0.177849033881895,
0.725667757128148));
#37985=CARTESIAN_POINT('Ctrl Pts',(-0.198481063804218,0.0204947628921387,
0.736778922176691));
#37986=CARTESIAN_POINT('Ctrl Pts',(-0.124900538360275,-0.155610486510929,
0.747890087225236));
#37987=CARTESIAN_POINT('Ctrl Pts',(0.0629534388405818,-0.189345273331751,
0.759001252273779));
#37988=CARTESIAN_POINT('Ctrl Pts',(0.193210332387941,-0.0498451146385645,
0.770112417322323));
#37989=CARTESIAN_POINT('Ctrl Pts',(0.146696077573226,0.135259117324623,
0.781223582370866));
#37990=CARTESIAN_POINT('Ctrl Pts',(-0.0340327079685797,0.196612671981249,
0.79233474741941));
#37991=CARTESIAN_POINT('Ctrl Pts',(-0.1836244378702,0.0780822246807544,
0.803445912467955));
#37992=CARTESIAN_POINT('Ctrl Pts',(-0.165215303905282,-0.111886868533138,
0.814557077516496));
#37993=CARTESIAN_POINT('Ctrl Pts',(0.00435188997620014,-0.199488919620082,
0.825668242565042));
#37994=CARTESIAN_POINT('Ctrl Pts',(0.169937471790653,-0.104575444878119,
0.836779407613584));
#37995=CARTESIAN_POINT('Ctrl Pts',(0.180044608624107,0.0860157363537389,
0.847890572662129));
#37996=CARTESIAN_POINT('Ctrl Pts',(0.0254261231896373,0.197909778109651,
0.859001737710672));
#37997=CARTESIAN_POINT('Ctrl Pts',(-0.152455119072723,0.128733075110866,
0.870112902759215));
#37998=CARTESIAN_POINT('Ctrl Pts',(-0.190852793819114,-0.058223527021699,
0.88122406780776));
#37999=CARTESIAN_POINT('Ctrl Pts',(-0.0546362687377931,-0.191910516224214,
0.892335232856302));
#38000=CARTESIAN_POINT('Ctrl Pts',(0.131567830711834,-0.150015578044556,
0.903446397904849));
#38001=CARTESIAN_POINT('Ctrl Pts',(0.197398469646436,0.0291309515284085,
0.914557562953389));
#38002=CARTESIAN_POINT('Ctrl Pts',(0.0826261660534066,0.181625122960423,
0.925668728001935));
#38003=CARTESIAN_POINT('Ctrl Pts',(-0.107742102476217,0.167947627257441,
0.936779893050478));
#38004=CARTESIAN_POINT('Ctrl Pts',(-0.199535447360731,0.000612240984059651,
0.947891058099021));
#38005=CARTESIAN_POINT('Ctrl Pts',(-0.108770683501224,-0.167283321944057,
0.959002223147566));
#38006=CARTESIAN_POINT('Ctrl Pts',(0.0815100495622697,-0.182128710017129,
0.970113388196108));
#38007=CARTESIAN_POINT('Ctrl Pts',(0.197216016898856,-0.0303417998080474,
0.981224553244654));
#38008=CARTESIAN_POINT('Ctrl Pts',(0.132485876137733,0.149205488514605,
0.992335718293196));
#38009=CARTESIAN_POINT('Ctrl Pts',(-0.0534574766563464,0.19224198146507,
1.00344688334174));
#38010=CARTESIAN_POINT('Ctrl Pts',(-0.190492099373632,0.0593939810525364,
1.01455804839028));
#38011=CARTESIAN_POINT('Ctrl Pts',(-0.153241862049827,-0.127795823782107,
1.02566921343883));
#38012=CARTESIAN_POINT('Ctrl Pts',(0.0242104795071353,-0.198060714106653,
1.03678037848737));
#38013=CARTESIAN_POINT('Ctrl Pts',(0.179514687230076,-0.0871215651841315,
1.04789154353591));
#38014=CARTESIAN_POINT('Ctrl Pts',(0.170573514980415,0.103535599219979,
1.05900270858446));
#38015=CARTESIAN_POINT('Ctrl Pts',(0.0055807119752709,0.199449035952863,
1.070113873633));
#38016=CARTESIAN_POINT('Ctrl Pts',(-0.164534610934924,0.112916549981001,
1.08122503868155));
#38017=CARTESIAN_POINT('Ctrl Pts',(-0.184082964550351,-0.0769881198690536,
1.09233620373009));
#38018=CARTESIAN_POINT('Ctrl Pts',(-0.0352713471113472,-0.196334799083268,
1.10344736877863));
#38019=CARTESIAN_POINT('Ctrl Pts',(0.145926315028038,-0.136283363878709,
1.11455853382718));
#38020=CARTESIAN_POINT('Ctrl Pts',(0.193386908374058,0.0489186345653294,
1.12566969887572));
#38021=CARTESIAN_POINT('Ctrl Pts',(0.107400308267113,0.141845702097726,
1.13307714224142));
#38022=CARTESIAN_POINT('Ctrl Pts',(0.0542488035626326,0.159880460833922,
1.13678086392426));
#38023=CARTESIAN_POINT('Ctrl Pts',(0.0903606778650208,-0.126612599672284,
-2.77555756156289E-16));
#38024=CARTESIAN_POINT('Ctrl Pts',(0.132452439122316,-0.0965726187415828,
0.00370372168284762));
#38025=CARTESIAN_POINT('Ctrl Pts',(0.183597970935092,0.00826171234133487,
0.0111111650485434));
#38026=CARTESIAN_POINT('Ctrl Pts',(0.0924933321163406,0.159015923519395,
0.0222223300970871));
#38027=CARTESIAN_POINT('Ctrl Pts',(-0.0833119343177651,0.163815447531815,
0.0333334951456308));
#38028=CARTESIAN_POINT('Ctrl Pts',(-0.182853304194564,0.018972784444937,
0.0444446601941745));
#38029=CARTESIAN_POINT('Ctrl Pts',(-0.115120619658919,-0.143350606534586,
0.0555558252427182));
#38030=CARTESIAN_POINT('Ctrl Pts',(0.0579488995883613,-0.174456230311225,
0.0666669902912619));
#38031=CARTESIAN_POINT('Ctrl Pts',(0.177994191588978,-0.0459827600750814,
0.0777781553398056));
#38032=CARTESIAN_POINT('Ctrl Pts',(0.135192905881154,0.124578720765632,
0.0888893203883492));
#38033=CARTESIAN_POINT('Ctrl Pts',(-0.0313001003158473,0.181151906168851,
0.100000485436893));
#38034=CARTESIAN_POINT('Ctrl Pts',(-0.169155304715778,0.0719912601030908,
0.111111650485437));
#38035=CARTESIAN_POINT('Ctrl Pts',(-0.152248128292804,-0.103037873939191,
0.12222281553398));
#38036=CARTESIAN_POINT('Ctrl Pts',(0.00395347168138628,-0.183794704008407,
0.133333980582524));
#38037=CARTESIAN_POINT('Ctrl Pts',(0.156537855283131,-0.0963955976349113,
0.144445145631068));
#38038=CARTESIAN_POINT('Ctrl Pts',(0.165903376979378,0.0791977165381959,
0.155556310679611));
#38039=CARTESIAN_POINT('Ctrl Pts',(0.0234812759114929,0.182331608910266,
0.166667475728155));
#38040=CARTESIAN_POINT('Ctrl Pts',(-0.1404241930473,0.118647569223042,0.177778640776699));
#38041=CARTESIAN_POINT('Ctrl Pts',(-0.175853385710917,-0.0535890369735552,
0.188889805825242));
#38042=CARTESIAN_POINT('Ctrl Pts',(-0.0503915664640746,-0.176796168665343,
0.200000970873786));
#38043=CARTESIAN_POINT('Ctrl Pts',(0.121174280763407,-0.138249741391359,
0.21111213592233));
#38044=CARTESIAN_POINT('Ctrl Pts',(0.181875888824183,0.0267835396201195,
0.222223300970874));
#38045=CARTESIAN_POINT('Ctrl Pts',(0.0761764071097843,0.167312138149853,
0.233334466019417));
#38046=CARTESIAN_POINT('Ctrl Pts',(-0.0992180579104728,0.154764252547341,
0.244445631067961));
#38047=CARTESIAN_POINT('Ctrl Pts',(-0.183836373538439,0.000620135891621234,
0.255556796116504));
#38048=CARTESIAN_POINT('Ctrl Pts',(-0.10025992194253,-0.154091352175446,
0.266667961165049));
#38049=CARTESIAN_POINT('Ctrl Pts',(0.0750458968510211,-0.167822257683237,
0.277779126213592));
#38050=CARTESIAN_POINT('Ctrl Pts',(0.181691053470019,-0.0280099604209337,
0.288890291262136));
#38051=CARTESIAN_POINT('Ctrl Pts',(0.122104229764526,0.137429086670804,
0.30000145631068));
#38052=CARTESIAN_POINT('Ctrl Pts',(-0.0491976593161155,0.177132117679823,
0.311112621359223));
#38053=CARTESIAN_POINT('Ctrl Pts',(-0.175487842108734,0.0547742098573187,
0.322223786407767));
#38054=CARTESIAN_POINT('Ctrl Pts',(-0.141221459472129,-0.117697477363263,
0.33333495145631));
#38055=CARTESIAN_POINT('Ctrl Pts',(0.0222506403513669,-0.18248590575151,
0.344446116504855));
#38056=CARTESIAN_POINT('Ctrl Pts',(0.165365282072159,-0.0803151310699741,
0.355557281553397));
#38057=CARTESIAN_POINT('Ctrl Pts',(0.157184646516792,0.0953372104320743,
0.366668446601942));
#38058=CARTESIAN_POINT('Ctrl Pts',(0.00519332482321354,0.183764050268212,
0.377779611650485));
#38059=CARTESIAN_POINT('Ctrl Pts',(-0.151549450798785,0.104062292672322,
0.388890776699029));
#38060=CARTESIAN_POINT('Ctrl Pts',(-0.169637268788223,-0.0708476804963227,
0.400001941747572));
#38061=CARTESIAN_POINT('Ctrl Pts',(-0.0325213021862407,-0.180938005122649,
0.411113106796117));
#38062=CARTESIAN_POINT('Ctrl Pts',(0.134348911316817,-0.125485325124609,
0.42222427184466));
#38063=CARTESIAN_POINT('Ctrl Pts',(0.178301209192838,0.0447758371671112,
0.433335436893204));
#38064=CARTESIAN_POINT('Ctrl Pts',(0.0591229481908682,0.174070887258225,
0.444446601941748));
#38065=CARTESIAN_POINT('Ctrl Pts',(-0.114147820789891,0.144105766028162,
0.455557766990291));
#38066=CARTESIAN_POINT('Ctrl Pts',(-0.182982967127054,-0.0177039694708382,
0.466668932038835));
#38067=CARTESIAN_POINT('Ctrl Pts',(-0.0844041411881997,-0.163316067010957,
0.477780097087378));
#38068=CARTESIAN_POINT('Ctrl Pts',(0.0913973507436636,-0.159507746114991,
0.488891262135923));
#38069=CARTESIAN_POINT('Ctrl Pts',(0.183577980123458,-0.00976329900371924,
0.500002427184466));
#38070=CARTESIAN_POINT('Ctrl Pts',(0.10780025055099,0.148913742733129,0.51111359223301));
#38071=CARTESIAN_POINT('Ctrl Pts',(-0.0666056105926533,0.17134727727987,
0.522224757281553));
#38072=CARTESIAN_POINT('Ctrl Pts',(-0.180072959150898,0.037012513779585,
0.533335922330097));
#38073=CARTESIAN_POINT('Ctrl Pts',(-0.128788747144402,-0.131185576198834,
0.544447087378641));
#38074=CARTESIAN_POINT('Ctrl Pts',(0.0403262995152723,-0.179359935217008,
0.555558252427184));
#38075=CARTESIAN_POINT('Ctrl Pts',(0.172546185411942,-0.0634350903950841,
0.566669417475728));
#38076=CARTESIAN_POINT('Ctrl Pts',(0.146900873501267,0.11052750860401,0.577780582524271));
#38077=CARTESIAN_POINT('Ctrl Pts',(-0.013146340126236,0.183366765077345,
0.588891747572816));
#38078=CARTESIAN_POINT('Ctrl Pts',(-0.161165762009075,0.0884409065403499,
0.600002912621358));
#38079=CARTESIAN_POINT('Ctrl Pts',(-0.16173211305994,-0.087400917608522,
0.611114077669903));
#38080=CARTESIAN_POINT('Ctrl Pts',(-0.0143272298638598,-0.183278278249422,
0.622225242718446));
#38081=CARTESIAN_POINT('Ctrl Pts',(0.146185859526926,-0.111471481859797,
0.63333640776699));
#38082=CARTESIAN_POINT('Ctrl Pts',(0.172951224644592,0.0623223129190563,
0.644447572815534));
#38083=CARTESIAN_POINT('Ctrl Pts',(0.0414808152398764,0.179096450999678,
0.655558737864077));
#38084=CARTESIAN_POINT('Ctrl Pts',(-0.127941039381778,0.1320124510626,0.666669902912621));
#38085=CARTESIAN_POINT('Ctrl Pts',(-0.180307640411694,-0.0358518005518811,
0.677781067961165));
#38086=CARTESIAN_POINT('Ctrl Pts',(-0.0677079673289082,-0.170914680334463,
0.68889223300971));
#38087=CARTESIAN_POINT('Ctrl Pts',(0.106838781720774,-0.149605051766532,
0.700003398058251));
#38088=CARTESIAN_POINT('Ctrl Pts',(0.183637062036826,0.00858057341481814,
0.711114563106797));
#38089=CARTESIAN_POINT('Ctrl Pts',(0.0924229284360449,0.1589156980696,0.722225728155339));
#38090=CARTESIAN_POINT('Ctrl Pts',(-0.0833503847528551,0.163856370505402,
0.733336893203883));
#38091=CARTESIAN_POINT('Ctrl Pts',(-0.182865130156443,0.0188822924059537,
0.744448058252428));
#38092=CARTESIAN_POINT('Ctrl Pts',(-0.115073714167466,-0.143367489694622,
0.75555922330097));
#38093=CARTESIAN_POINT('Ctrl Pts',(0.0580004387659595,-0.174448118065669,
0.766670388349515));
#38094=CARTESIAN_POINT('Ctrl Pts',(0.17800908511122,-0.0459234407622611,
0.777781553398057));
#38095=CARTESIAN_POINT('Ctrl Pts',(0.135154441460109,0.124617309179735,
0.788892718446602));
#38096=CARTESIAN_POINT('Ctrl Pts',(-0.0313551099181417,0.181143738163968,
0.800003883495145));
#38097=CARTESIAN_POINT('Ctrl Pts',(-0.169177381899564,0.0719389341505889,
0.81111504854369));
#38098=CARTESIAN_POINT('Ctrl Pts',(-0.152216626984007,-0.103083923397808,
0.822226213592232));
#38099=CARTESIAN_POINT('Ctrl Pts',(0.00400949547363229,-0.183793690702293,
0.833337378640777));
#38100=CARTESIAN_POINT('Ctrl Pts',(0.156567267939011,-0.0963477420579929,
0.844448543689319));
#38101=CARTESIAN_POINT('Ctrl Pts',(0.165879203582308,0.0792482593671729,
0.855559708737864));
#38102=CARTESIAN_POINT('Ctrl Pts',(0.0234256671005791,0.182338791618694,
0.866670873786407));
#38103=CARTESIAN_POINT('Ctrl Pts',(-0.140460377720211,0.118604717671243,
0.877782038834952));
#38104=CARTESIAN_POINT('Ctrl Pts',(-0.175837031067501,-0.0536426631484242,
0.888893203883495));
#38105=CARTESIAN_POINT('Ctrl Pts',(-0.0503376402892206,-0.17681153483915,
0.900004368932038));
#38106=CARTESIAN_POINT('Ctrl Pts',(0.12121644264892,-0.138212772940753,
0.911115533980582));
#38107=CARTESIAN_POINT('Ctrl Pts',(0.181867711471885,0.026839009932345,
0.922226699029127));
#38108=CARTESIAN_POINT('Ctrl Pts',(0.0761253709552246,0.167335367481701,
0.933337864077668));
#38109=CARTESIAN_POINT('Ctrl Pts',(-0.099265255914171,0.154733978795034,
0.944449029126215));
#38110=CARTESIAN_POINT('Ctrl Pts',(-0.18383655777075,0.000564071579882353,
0.955560194174756));
#38111=CARTESIAN_POINT('Ctrl Pts',(-0.100212911067809,-0.154121939161292,
0.966671359223301));
#38112=CARTESIAN_POINT('Ctrl Pts',(0.0750970673805211,-0.167799333720618,
0.977782524271844));
#38113=CARTESIAN_POINT('Ctrl Pts',(0.181699613594968,-0.0279545920640164,
0.988893689320389));
#38114=CARTESIAN_POINT('Ctrl Pts',(0.122062258834496,0.137466418983892,
1.00000485436893));
#38115=CARTESIAN_POINT('Ctrl Pts',(-0.0492515922639386,0.177116921324136,
1.01111601941748));
#38116=CARTESIAN_POINT('Ctrl Pts',(-0.175504715049764,0.0547210291375423,
1.02222718446602));
#38117=CARTESIAN_POINT('Ctrl Pts',(-0.14118522196555,-0.1177412066494,1.03333834951456));
#38118=CARTESIAN_POINT('Ctrl Pts',(0.0223056668548975,-0.182477852394609,
1.04444951456311));
#38119=CARTESIAN_POINT('Ctrl Pts',(0.165390974917898,-0.0802670846854376,
1.05556067961165));
#38120=CARTESIAN_POINT('Ctrl Pts',(0.157153269033781,0.0953897085409752,
1.06667184466019));
#38121=CARTESIAN_POINT('Ctrl Pts',(0.00514163720288116,0.183756944970195,
1.07778300970874));
#38122=CARTESIAN_POINT('Ctrl Pts',(-0.151589489028199,0.104032592396117,
1.08889417475728));
#38123=CARTESIAN_POINT('Ctrl Pts',(-0.169599832986023,-0.0709309104380943,
1.10000533980583));
#38124=CARTESIAN_POINT('Ctrl Pts',(-0.0324962964057439,-0.180887727526569,
1.11111650485437));
#38125=CARTESIAN_POINT('Ctrl Pts',(0.134445241673909,-0.125560970886474,
1.12222766990291));
#38126=CARTESIAN_POINT('Ctrl Pts',(0.178171768593789,0.0450698535437549,
1.13333883495146));
#38127=CARTESIAN_POINT('Ctrl Pts',(0.0989503531151977,0.130685679928735,
1.14074627831715));
#38128=CARTESIAN_POINT('Ctrl Pts',(0.0499806597877626,0.147301514408983,
1.14445));
#38129=CARTESIAN_POINT('',(0.0903606778650206,-0.126612599672284,0.));
#38130=CARTESIAN_POINT('Ctrl Pts',(0.0903606778650208,-0.126612599672284,
-2.77555756156289E-16));
#38131=CARTESIAN_POINT('Ctrl Pts',(0.132452439122316,-0.0965726187415828,
0.00370372168284762));
#38132=CARTESIAN_POINT('Ctrl Pts',(0.183597970935092,0.00826171234133487,
0.0111111650485434));
#38133=CARTESIAN_POINT('Ctrl Pts',(0.0924933321163406,0.159015923519395,
0.0222223300970871));
#38134=CARTESIAN_POINT('Ctrl Pts',(-0.0833119343177651,0.163815447531815,
0.0333334951456308));
#38135=CARTESIAN_POINT('Ctrl Pts',(-0.15310616378989,0.0622578531632503,
0.0411241775931451));
#38136=CARTESIAN_POINT('Ctrl Pts',(-0.155772922446558,0.00543356393242454,
0.0452111383578116));
#38137=CARTESIAN_POINT('Ctrl Pts',(-0.155735926886437,0.000101346774827265,
0.0455943774396301));
#38138=CARTESIAN_POINT('Ctrl Pts',(0.0863567639152676,0.175641488315944,
2.2659825404947E-17));
#38139=CARTESIAN_POINT('Ctrl Pts',(0.0902605506355985,0.173244147111074,
2.45989142876686E-17));
#38140=CARTESIAN_POINT('Ctrl Pts',(0.0940681517855526,0.170703362163956,
1.50959816364938E-17));
#38141=CARTESIAN_POINT('Ctrl Pts',(0.0977705169885396,0.168018661523996,
1.10588621593521E-17));
#38142=CARTESIAN_POINT('Ctrl Pts',(0.104919852250204,0.162834455239647,
2.72100915479622E-18));
#38143=CARTESIAN_POINT('Ctrl Pts',(0.111677400716997,0.157113958337607,
-2.16691070983975E-17));
#38144=CARTESIAN_POINT('Ctrl Pts',(0.118012246833275,0.150919901422416,
-3.33934269125535E-17));
#38145=CARTESIAN_POINT('Ctrl Pts',(0.122832506482077,0.146206769948873,
-4.2314601108814E-17));
#38146=CARTESIAN_POINT('Ctrl Pts',(0.127411584310215,0.141213843322959,
-4.34283416288416E-17));
#38147=CARTESIAN_POINT('Ctrl Pts',(0.131710542479305,0.135995360136636,
-4.0766001685455E-17));
#38148=CARTESIAN_POINT('Ctrl Pts',(0.136227531634889,0.130512210258439,
-3.79686353981478E-17));
#38149=CARTESIAN_POINT('Ctrl Pts',(0.140440157604184,0.124776412163605,
1.15313389293564E-17));
#38150=CARTESIAN_POINT('Ctrl Pts',(0.144331170139148,0.11882042578862,3.72965547335014E-17));
#38151=CARTESIAN_POINT('Ctrl Pts',(0.147802837134673,0.113506333084464,
6.02849796064744E-17));
#38152=CARTESIAN_POINT('Ctrl Pts',(0.15101843405387,0.108016870008689,-1.53625880027527E-18));
#38153=CARTESIAN_POINT('Ctrl Pts',(0.153962315598392,0.102374391558266,
-8.67361737988404E-18));
#38154=CARTESIAN_POINT('Ctrl Pts',(0.15571005357274,0.0990245373918854,
-1.29109592829026E-17));
#38155=CARTESIAN_POINT('Ctrl Pts',(0.157357576324963,0.0956291376942575,
-3.44593994380303E-18));
#38156=CARTESIAN_POINT('Ctrl Pts',(0.158902506880511,0.0921936740973187,
-6.07153216591882E-18));
#38157=CARTESIAN_POINT('Ctrl Pts',(0.163908283820673,0.0810623229886477,
-1.45787941606636E-17));
#38158=CARTESIAN_POINT('Ctrl Pts',(0.167841697827597,0.0695089356622268,
-9.75260753403157E-18));
#38159=CARTESIAN_POINT('Ctrl Pts',(0.170598119604662,0.0576980955231356,
-5.20417042793042E-18));
#38160=CARTESIAN_POINT('Ctrl Pts',(0.171984491688748,0.0517577059954232,
-2.91648489207139E-18));
#38161=CARTESIAN_POINT('Ctrl Pts',(0.173072324320188,0.0457521241966622,
1.08654590748341E-17));
#38162=CARTESIAN_POINT('Ctrl Pts',(0.173843127025583,0.0397030009933723,
1.73472347597681E-17));
#38163=CARTESIAN_POINT('Ctrl Pts',(0.174324086814962,0.0359285136940646,
2.13916853648473E-17));
#38164=CARTESIAN_POINT('Ctrl Pts',(0.17468129632341,0.0321360477424029,
-3.73379012875618E-17));
#38165=CARTESIAN_POINT('Ctrl Pts',(0.174909438673913,0.0283479136595781,
-3.46944695195361E-17));
#38166=CARTESIAN_POINT('Ctrl Pts',(0.175317247780942,0.0215765466853118,
-2.99692812919358E-17));
#38167=CARTESIAN_POINT('Ctrl Pts',(0.175315000224248,0.0148063200599795,
-5.50593613673983E-17));
#38168=CARTESIAN_POINT('Ctrl Pts',(0.174882170147482,0.00806701752180915,
-4.68375338513738E-17));
#38169=CARTESIAN_POINT('Ctrl Pts',(0.174454769721774,0.00141225638482493,
-4.0453568795602E-17));
#38170=CARTESIAN_POINT('Ctrl Pts',(0.173607423807277,-0.00521244743448051,
5.53912001912299E-18));
#38171=CARTESIAN_POINT('Ctrl Pts',(0.172357876958299,-0.0117762500451153,
6.93889390390723E-18));
#38172=CARTESIAN_POINT('Ctrl Pts',(0.171266545977134,-0.0175089531839406,
8.16143038450564E-18));
#38173=CARTESIAN_POINT('Ctrl Pts',(0.169868307866471,-0.0231952127882146,
5.24172218001205E-19));
#38174=CARTESIAN_POINT('Ctrl Pts',(0.168172344307035,-0.0288124942050995,
-3.46944695195361E-18));
#38175=CARTESIAN_POINT('Ctrl Pts',(0.167269600009596,-0.0318025164482014,
-5.59521015704244E-18));
#38176=CARTESIAN_POINT('Ctrl Pts',(0.166282932031305,-0.0347708579305845,
-1.1797187803688E-17));
#38177=CARTESIAN_POINT('Ctrl Pts',(0.165217237950495,-0.0377059593473793,
-8.67361737988404E-18));
#38178=CARTESIAN_POINT('Ctrl Pts',(0.161836480623691,-0.047017135789496,
1.23544919580411E-18));
#38179=CARTESIAN_POINT('Ctrl Pts',(0.157654897120342,-0.0560198074489911,
-1.7088045241211E-17));
#38180=CARTESIAN_POINT('Ctrl Pts',(0.152731837788828,-0.0646106508942882,
1.38777878078145E-17));
#38181=CARTESIAN_POINT('Ctrl Pts',(0.14995806869425,-0.0694509370741418,
3.13246770113308E-17));
#38182=CARTESIAN_POINT('Ctrl Pts',(0.146948492244732,-0.074160201986225,
-2.50126624213863E-18));
#38183=CARTESIAN_POINT('Ctrl Pts',(0.143711118647294,-0.0787168991005189,
3.46944695195361E-18));
#38184=CARTESIAN_POINT('Ctrl Pts',(0.141667380230334,-0.0815935201226661,
7.2387295398745E-18));
#38185=CARTESIAN_POINT('Ctrl Pts',(0.139532823645962,-0.0844092886780934,
1.73900611772481E-17));
#38186=CARTESIAN_POINT('Ctrl Pts',(0.137309196652862,-0.08715819230643,
2.08166817117217E-17));
#38187=CARTESIAN_POINT('Ctrl Pts',(0.135173374337891,-0.0897985495827733,
2.41079947894884E-17));
#38188=CARTESIAN_POINT('Ctrl Pts',(0.132961417486925,-0.0923697150592745,
-3.29131307776674E-18));
#38189=CARTESIAN_POINT('Ctrl Pts',(0.130676581353388,-0.0948665968574491,
0.));
#38190=CARTESIAN_POINT('Ctrl Pts',(0.123427275316167,-0.10278867933332,
1.04426463739872E-17));
#38191=CARTESIAN_POINT('Ctrl Pts',(0.115443266551879,-0.109969536302748,
2.37276977285196E-17));
#38192=CARTESIAN_POINT('Ctrl Pts',(0.106786977446893,-0.116251471062968,
2.77555756156289E-17));
#38193=CARTESIAN_POINT('Ctrl Pts',(0.101553949468808,-0.120049119218897,
3.01905679570255E-17));
#38194=CARTESIAN_POINT('Ctrl Pts',(0.0960747579407472,-0.123517461158967,
2.18989005301202E-17));
#38195=CARTESIAN_POINT('Ctrl Pts',(0.0903606778650241,-0.126612599672281,
2.08166817117217E-17));
#38196=CARTESIAN_POINT('Ctrl Pts',(0.188079991776263,-0.0516378774142081,
1.1046));
#38197=CARTESIAN_POINT('Ctrl Pts',(0.179754570390634,-0.0821182550519846,
1.1028067538919));
#38198=CARTESIAN_POINT('Ctrl Pts',(0.164446793279769,-0.110682480125595,
1.1010135077838));
#38199=CARTESIAN_POINT('Ctrl Pts',(0.143091597726206,-0.133587557506818,
1.09922026167571));
#38200=CARTESIAN_POINT('Ctrl Pts',(0.0989851583166799,-0.180895080641009,
1.09551653999286));
#38201=CARTESIAN_POINT('Ctrl Pts',(0.0290818548970629,-0.204062011418838,
1.09181281831001));
#38202=CARTESIAN_POINT('Ctrl Pts',(-0.0345744266721549,-0.19262440956347,
1.08810909662716));
#38203=CARTESIAN_POINT('Ctrl Pts',(-0.0982307082413709,-0.181186807708102,
1.08440537494431));
#38204=CARTESIAN_POINT('Ctrl Pts',(-0.155639967960188,-0.135144673219537,
1.08070165326147));
#38205=CARTESIAN_POINT('Ctrl Pts',(-0.180573868997825,-0.0754924386616321,
1.07699793157862));
#38206=CARTESIAN_POINT('Ctrl Pts',(-0.190472245868201,-0.0518114150655666,
1.07552761078989));
#38207=CARTESIAN_POINT('Ctrl Pts',(-0.195252608806662,-0.0259854826956367,
1.07405729000116));
#38208=CARTESIAN_POINT('Ctrl Pts',(-0.195129684289216,-0.000113636086278679,
1.07258696921242));
#38209=CARTESIAN_POINT('Origin',(0.,0.,-0.129405622560369));
#38210=CARTESIAN_POINT('',(-0.0903606778650173,-0.126612599672286,0.));
#38211=CARTESIAN_POINT('Ctrl Pts',(-0.0905549614304886,-0.126792015305981,
1.24276674021151E-16));
#38212=CARTESIAN_POINT('Ctrl Pts',(-0.0513706458239086,-0.154472437079514,
0.00344950590738082));
#38213=CARTESIAN_POINT('Ctrl Pts',(0.0587535178885047,-0.172169358136003,
0.0106052258091336));
#38214=CARTESIAN_POINT('Ctrl Pts',(0.177508460417327,-0.0479721809770191,
0.0214671597052585));
#38215=CARTESIAN_POINT('Ctrl Pts',(0.13650560094313,0.123222299189869,0.0325858016883748));
#38216=CARTESIAN_POINT('Ctrl Pts',(-0.0295638381403906,0.181478253869214,
0.043704443671491));
#38217=CARTESIAN_POINT('Ctrl Pts',(-0.141307745535963,0.0946781319192958,
0.0526443839621562));
#38218=CARTESIAN_POINT('Ctrl Pts',(-0.155414936746312,0.0214718667413076,
0.0578781102584494));
#38219=CARTESIAN_POINT('Ctrl Pts',(-0.155326046963413,7.29270061605551E-5,
0.0594056225603705));
#38220=CARTESIAN_POINT('Origin',(0.,0.,0.));
#38221=CARTESIAN_POINT('Ctrl Pts',(-0.0685825729128748,0.139614588036674,
-0.0230074082272066));
#38222=CARTESIAN_POINT('Ctrl Pts',(-0.115028016933624,0.116799292759742,
-0.0193011942328345));
#38223=CARTESIAN_POINT('Ctrl Pts',(-0.182555218707277,0.0215691441263552,
-0.0118887662440903));
#38224=CARTESIAN_POINT('Ctrl Pts',(-0.116942936218886,-0.142059634545264,
-0.000770124260974049));
#38225=CARTESIAN_POINT('Ctrl Pts',(0.0559468948314244,-0.175104601534012,
0.0103485177221422));
#38226=CARTESIAN_POINT('Ctrl Pts',(0.177508460417327,-0.0479721809770191,
0.0214671597052585));
#38227=CARTESIAN_POINT('Ctrl Pts',(0.13650560094313,0.123222299189869,0.0325858016883748));
#38228=CARTESIAN_POINT('Ctrl Pts',(-0.0295638381403906,0.181478253869214,
0.043704443671491));
#38229=CARTESIAN_POINT('Ctrl Pts',(-0.168540213790592,0.0735245708832444,
0.0548230856546073));
#38230=CARTESIAN_POINT('Ctrl Pts',(-0.153132379752993,-0.101797781965797,
0.0659417276377235));
#38231=CARTESIAN_POINT('Ctrl Pts',(0.00255447675030308,-0.183860034663711,
0.0770603696208398));
#38232=CARTESIAN_POINT('Ctrl Pts',(0.155899683301632,-0.0975032021788082,
0.0881790116039561));
#38233=CARTESIAN_POINT('Ctrl Pts',(0.166434877052597,0.0781732535368643,
0.0992976535870723));
#38234=CARTESIAN_POINT('Ctrl Pts',(0.0245080507541896,0.182238325373942,
0.110416295570189));
#38235=CARTESIAN_POINT('Ctrl Pts',(-0.139868975820189,0.119365863723167,
0.121534937553305));
#38236=CARTESIAN_POINT('Ctrl Pts',(-0.176120077222934,-0.0528512641939849,
0.132653579536421));
#38237=CARTESIAN_POINT('Ctrl Pts',(-0.0510374815939226,-0.176654153931159,
0.143772221519537));
#38238=CARTESIAN_POINT('Ctrl Pts',(0.120797626960931,-0.138634273102519,
0.154890863502654));
#38239=CARTESIAN_POINT('Ctrl Pts',(0.181976886629041,0.0263806680570579,
0.16600950548577));
#38240=CARTESIAN_POINT('Ctrl Pts',(0.0764574137846417,0.167229745635935,
0.177128147468886));
#38241=CARTESIAN_POINT('Ctrl Pts',(-0.0991003621173195,0.154889135395602,
0.188246789452002));
#38242=CARTESIAN_POINT('Ctrl Pts',(-0.183877909581896,0.000663349951290586,
0.199365431435119));
#38243=CARTESIAN_POINT('Ctrl Pts',(-0.100215313155719,-0.154170088892816,
0.210484073418235));
#38244=CARTESIAN_POINT('Ctrl Pts',(0.0752488571272716,-0.167777039880966,
0.221602715401351));
#38245=CARTESIAN_POINT('Ctrl Pts',(0.181781810074028,-0.0276929424335053,
0.232721357384467));
#38246=CARTESIAN_POINT('Ctrl Pts',(0.121794738393109,0.137759091140133,
0.243839999367584));
#38247=CARTESIAN_POINT('Ctrl Pts',(-0.0497615974795104,0.177017821004958,
0.2549586413507));
#38248=CARTESIAN_POINT('Ctrl Pts',(-0.175734151264734,0.0541205469518692,
0.266077283333817));
#38249=CARTESIAN_POINT('Ctrl Pts',(-0.140726598433086,-0.11835349598584,
0.277195925316932));
#38250=CARTESIAN_POINT('Ctrl Pts',(0.0231926238140432,-0.182410602009977,
0.288314567300049));
#38251=CARTESIAN_POINT('Ctrl Pts',(0.165866396469461,-0.0793716828903688,
0.299433209283165));
#38252=CARTESIAN_POINT('Ctrl Pts',(0.156599354026699,0.096375141196464,
0.310551851266282));
#38253=CARTESIAN_POINT('Ctrl Pts',(0.00388050940998321,0.183838154825996,
0.321670493249398));
#38254=CARTESIAN_POINT('Ctrl Pts',(-0.152393050178991,0.102897443019027,
0.332789135232514));
#38255=CARTESIAN_POINT('Ctrl Pts',(-0.169067964401488,-0.0723017906820314,
0.34390777721563));
#38256=CARTESIAN_POINT('Ctrl Pts',(-0.0308692884081366,-0.181269447386996,
0.355026419198746));
#38257=CARTESIAN_POINT('Ctrl Pts',(0.135606994996762,-0.124186426112907,
0.366145061181863));
#38258=CARTESIAN_POINT('Ctrl Pts',(0.177861387826841,0.0466567491694538,
0.377263703164979));
#38259=CARTESIAN_POINT('Ctrl Pts',(0.0571870330903418,0.174760318061885,
0.388382345148095));
#38260=CARTESIAN_POINT('Ctrl Pts',(-0.115873124952358,0.142775853828764,
0.399500987131212));
#38261=CARTESIAN_POINT('Ctrl Pts',(-0.182788473512851,-0.0199974866820836,
0.410619629114327));
#38262=CARTESIAN_POINT('Ctrl Pts',(-0.0822616502622442,-0.164452261823584,
0.421738271097444));
#38263=CARTESIAN_POINT('Ctrl Pts',(0.0936204134582059,-0.158261630557358,
0.43285691308056));
#38264=CARTESIAN_POINT('Ctrl Pts',(0.183742116834086,-0.00709647969689106,
0.443975555063676));
#38265=CARTESIAN_POINT('Ctrl Pts',(0.10554806974386,0.150569354438759,0.455094197046793));
#38266=CARTESIAN_POINT('Ctrl Pts',(-0.0693325883166112,0.170307127625589,
0.466212839029909));
#38267=CARTESIAN_POINT('Ctrl Pts',(-0.180701587562324,0.0340361833232659,
0.477331481013025));
#38268=CARTESIAN_POINT('Ctrl Pts',(-0.126540093064824,-0.133413381524886,
0.488450122996142));
#38269=CARTESIAN_POINT('Ctrl Pts',(0.0435376164803608,-0.17865050090601,
0.499568764979258));
#38270=CARTESIAN_POINT('Ctrl Pts',(0.173732980498774,-0.0602360109052031,
0.510687406962374));
#38271=CARTESIAN_POINT('Ctrl Pts',(0.144781397169404,0.113357278356683,
0.521806048945491));
#38272=CARTESIAN_POINT('Ctrl Pts',(-0.0167962271460079,0.183110382765203,
0.532924690928607));
#38273=CARTESIAN_POINT('Ctrl Pts',(-0.162987778710162,0.0851264325217889,
0.544043332911723));
#38274=CARTESIAN_POINT('Ctrl Pts',(-0.159875453933454,-0.0908370230265797,
0.555161974894839));
#38275=CARTESIAN_POINT('Ctrl Pts',(-0.0103102773360761,-0.183589824620028,
0.566280616877956));
#38276=CARTESIAN_POINT('Ctrl Pts',(0.14869956060099,-0.108166382022474,
0.577399258861071));
#38277=CARTESIAN_POINT('Ctrl Pts',(0.171494149863546,0.0663421591850832,
0.588517900844189));
#38278=CARTESIAN_POINT('Ctrl Pts',(0.0371926577693494,0.180078404398782,
0.599636542827304));
#38279=CARTESIAN_POINT('Ctrl Pts',(-0.1311789224034,0.128855018683177,0.610755184810421));
#38280=CARTESIAN_POINT('Ctrl Pts',(-0.179384918603911,-0.0404051543769803,
0.621873826793537));
#38281=CARTESIAN_POINT('Ctrl Pts',(-0.0632665469493242,-0.172652453095426,
0.632992468776653));
#38282=CARTESIAN_POINT('Ctrl Pts',(0.110806726459172,-0.146742614445027,
0.644111110759769));
#38283=CARTESIAN_POINT('Ctrl Pts',(0.183376231205259,0.0135898253011021,
0.655229752742886));
#38284=CARTESIAN_POINT('Ctrl Pts',(0.0879651525947856,0.161473395492061,
0.666348394726001));
#38285=CARTESIAN_POINT('Ctrl Pts',(-0.0880258220622017,0.161440330069759,
0.677467036709119));
#38286=CARTESIAN_POINT('Ctrl Pts',(-0.183381324808445,0.013520918395534,
0.688585678692234));
#38287=CARTESIAN_POINT('Ctrl Pts',(-0.11075157823663,-0.146784241118916,
0.699704320675351));
#38288=CARTESIAN_POINT('Ctrl Pts',(0.0633314188332071,-0.172628667698419,
0.710822962658467));
#38289=CARTESIAN_POINT('Ctrl Pts',(0.17940008868909,-0.0403377453646542,
0.721941604641583));
#38290=CARTESIAN_POINT('Ctrl Pts',(0.131130494233742,0.128904301731096,
0.733060246624699));
#38291=CARTESIAN_POINT('Ctrl Pts',(-0.0372603218894873,0.180064416072257,
0.744178888607816));
#38292=CARTESIAN_POINT('Ctrl Pts',(-0.171519066664489,0.0662777133981789,
0.755297530590932));
#38293=CARTESIAN_POINT('Ctrl Pts',(-0.148658905212271,-0.108222250133236,
0.766416172574049));
#38294=CARTESIAN_POINT('Ctrl Pts',(0.0103792628149562,-0.18358593744105,
0.777534814557165));
#38295=CARTESIAN_POINT('Ctrl Pts',(0.159909575810308,-0.0907769413831382,
0.78865345654028));
#38296=CARTESIAN_POINT('Ctrl Pts',(0.162955779866738,0.0851876712390422,
0.799772098523398));
#38297=CARTESIAN_POINT('Ctrl Pts',(0.0167274199086701,0.183116681231986,
0.810890740506512));
#38298=CARTESIAN_POINT('Ctrl Pts',(-0.144823982381472,0.11330286690894,
0.82200938248963));
#38299=CARTESIAN_POINT('Ctrl Pts',(-0.173710333792674,-0.0603012890298399,
0.833128024472746));
#38300=CARTESIAN_POINT('Ctrl Pts',(-0.0434704832044991,-0.178666848096071,
0.844246666455862));
#38301=CARTESIAN_POINT('Ctrl Pts',(0.126590215885116,-0.133365823077974,
0.855365308438979));
#38302=CARTESIAN_POINT('Ctrl Pts',(0.18068878531032,0.0341040818691465,
0.866483950422094));
#38303=CARTESIAN_POINT('Ctrl Pts',(0.069268588294083,0.170333168137465,
0.877602592405212));
#38304=CARTESIAN_POINT('Ctrl Pts',(-0.105604640517969,0.15052968290502,
0.888721234388326));
#38305=CARTESIAN_POINT('Ctrl Pts',(-0.183739437498563,-0.00716552286239433,
0.899839876371444));
#38306=CARTESIAN_POINT('Ctrl Pts',(-0.0935609375970031,-0.15829679799695,
0.91095851835456));
#38307=CARTESIAN_POINT('Ctrl Pts',(0.0823234386500799,-0.164421340203127,
0.922077160337675));
#38308=CARTESIAN_POINT('Ctrl Pts',(0.182795976495949,-0.0199287985657338,
0.933195802320793));
#38309=CARTESIAN_POINT('Ctrl Pts',(0.115819463928053,0.142819381470141,
0.944314444303908));
#38310=CARTESIAN_POINT('Ctrl Pts',(-0.0572526917402423,0.174738822826618,
0.955433086287024));
#38311=CARTESIAN_POINT('Ctrl Pts',(-0.177878918025408,0.046589901053406,
0.966551728270142));
#38312=CARTESIAN_POINT('Ctrl Pts',(-0.135560300066214,-0.124237352171324,
0.977670370253256));
#38313=CARTESIAN_POINT('Ctrl Pts',(0.0309373610575528,-0.181257875466721,
0.988789012236375));
#38314=CARTESIAN_POINT('Ctrl Pts',(0.169095195914933,-0.0722381792257861,
0.999907654219489));
#38315=CARTESIAN_POINT('Ctrl Pts',(0.152354231364944,0.102954552944809,
1.01102629620261));
#38316=CARTESIAN_POINT('Ctrl Pts',(-0.00394931635484403,0.183836962465064,
1.02214493818572));
#38317=CARTESIAN_POINT('Ctrl Pts',(-0.156636075542215,0.0963157594965877,
1.03326358016884));
#38318=CARTESIAN_POINT('Ctrl Pts',(-0.165835572967195,-0.0794329933758677,
1.04438222215196));
#38319=CARTESIAN_POINT('Ctrl Pts',(-0.0231259578302998,-0.182421227428175,
1.05550086413507));
#38320=CARTESIAN_POINT('Ctrl Pts',(0.140774638007895,-0.11829694620695,
1.06661950611819));
#38321=CARTESIAN_POINT('Ctrl Pts',(0.175706993010233,0.0541796064983141,
1.07773814810131));
#38322=CARTESIAN_POINT('Ctrl Pts',(0.0497080432048737,0.177049779856472,
1.08885679008442));
#38323=CARTESIAN_POINT('Ctrl Pts',(-0.121871201614337,0.137688031013954,
1.09997543206754));
#38324=CARTESIAN_POINT('Ctrl Pts',(-0.181724153253684,-0.027712968875509,
1.11109407405065));
#38325=CARTESIAN_POINT('Ctrl Pts',(-0.075277483453787,-0.167898453189698,
1.12221271603377));
#38326=CARTESIAN_POINT('Ctrl Pts',(0.100462758039806,-0.153944373403644,
1.13333135801688));
#38327=CARTESIAN_POINT('Ctrl Pts',(0.155754888396286,-0.0511266487217653,
1.14074378600563));
#38328=CARTESIAN_POINT('Ctrl Pts',(0.155548765964692,0.000619602180124784,
1.14445));
#38329=CARTESIAN_POINT('Ctrl Pts',(-0.074439243930934,0.151537102412034,
-0.0153382721514711));
#38330=CARTESIAN_POINT('Ctrl Pts',(-0.124850938769699,0.126773474301532,
-0.011632058157099));
#38331=CARTESIAN_POINT('Ctrl Pts',(-0.198144687185762,0.0234110607521693,
-0.0042196301683548));
#38332=CARTESIAN_POINT('Ctrl Pts',(-0.126929384324154,-0.154190945884872,
0.00689901181476148));
#38333=CARTESIAN_POINT('Ctrl Pts',(0.0607245306591998,-0.190057817801302,
0.0180176537978778));
#38334=CARTESIAN_POINT('Ctrl Pts',(0.192666956394248,-0.0520688088821623,
0.029136295780994));
#38335=CARTESIAN_POINT('Ctrl Pts',(0.148162620545796,0.133744979191402,
0.0402549377641103));
#38336=CARTESIAN_POINT('Ctrl Pts',(-0.0320884689126903,0.19697575395855,
0.0513735797472264));
#38337=CARTESIAN_POINT('Ctrl Pts',(-0.182932858212653,0.0798032683003624,
0.0624922217303428));
#38338=CARTESIAN_POINT('Ctrl Pts',(-0.166209258212561,-0.110490895887015,
0.0736108637134591));
#38339=CARTESIAN_POINT('Ctrl Pts',(0.00277261860929502,-0.199560929084259,
0.0847295056965753));
#38340=CARTESIAN_POINT('Ctrl Pts',(0.169212878157669,-0.10582957656395,
0.0958481476796916));
#38341=CARTESIAN_POINT('Ctrl Pts',(0.180647734334385,0.0848489294255244,
0.106966789662808));
#38342=CARTESIAN_POINT('Ctrl Pts',(0.0266009379770665,0.197800732458805,
0.118085431645924));
#38343=CARTESIAN_POINT('Ctrl Pts',(-0.151813213871049,0.12955921992025,
0.129204073629041));
#38344=CARTESIAN_POINT('Ctrl Pts',(-0.191160010957712,-0.0573645458357494,
0.140322715612156));
#38345=CARTESIAN_POINT('Ctrl Pts',(-0.0553958736254638,-0.191739695630841,
0.151441357595273));
#38346=CARTESIAN_POINT('Ctrl Pts',(0.131113249878304,-0.150473072594935,
0.162559999578389));
#38347=CARTESIAN_POINT('Ctrl Pts',(0.19751696791516,0.0286334691329668,
0.173678641561505));
#38348=CARTESIAN_POINT('Ctrl Pts',(0.0829865639814035,0.181510481441338,
0.184797283544622));
#38349=CARTESIAN_POINT('Ctrl Pts',(-0.107563127424026,0.168116033596642,
0.195915925527738));
#38350=CARTESIAN_POINT('Ctrl Pts',(-0.199580330447296,0.000719997322039096,
0.207034567510854));
#38351=CARTESIAN_POINT('Ctrl Pts',(-0.108773290717609,-0.167335583465575,
0.218153209493971));
#38352=CARTESIAN_POINT('Ctrl Pts',(0.0816748015321165,-0.182104512374819,
0.229271851477087));
#38353=CARTESIAN_POINT('Ctrl Pts',(0.197305232620797,-0.0300578063700233,
0.240390493460203));
#38354=CARTESIAN_POINT('Ctrl Pts',(0.132195510545613,0.149523153675082,
0.251509135443319));
#38355=CARTESIAN_POINT('Ctrl Pts',(-0.054011034229875,0.192134418384253,
0.262627777426435));
#38356=CARTESIAN_POINT('Ctrl Pts',(-0.190741128502276,0.0587422201459823,
0.273746419409552));
#38357=CARTESIAN_POINT('Ctrl Pts',(-0.152744073944838,-0.128460400121777,
0.284865061392668));
#38358=CARTESIAN_POINT('Ctrl Pts',(0.0251731789602741,-0.19798772081443,
0.295983703375785));
#38359=CARTESIAN_POINT('Ctrl Pts',(0.180030707836241,-0.0861496997406464,
0.3071023453589));
#38360=CARTESIAN_POINT('Ctrl Pts',(0.169972297898904,0.104605183790867,
0.318220987342017));
#38361=CARTESIAN_POINT('Ctrl Pts',(0.00421188903066005,0.199537180797957,
0.329339629325133));
#38362=CARTESIAN_POINT('Ctrl Pts',(-0.165406792919015,0.111684463493277,
0.34045827130825));
#38363=CARTESIAN_POINT('Ctrl Pts',(-0.183505676565636,-0.0784760676748057,
0.351576913291366));
#38364=CARTESIAN_POINT('Ctrl Pts',(-0.0335053992900935,-0.196749116257395,
0.362695555274482));
#38365=CARTESIAN_POINT('Ctrl Pts',(0.147187277329603,-0.134791438607496,
0.373814197257599));
#38366=CARTESIAN_POINT('Ctrl Pts',(0.193050022360002,0.0506410445822938,
0.384932839240714));
#38367=CARTESIAN_POINT('Ctrl Pts',(0.0620705716495424,0.189684133929807,
0.396051481223831));
#38368=CARTESIAN_POINT('Ctrl Pts',(-0.125768215554202,0.154968327363698,
0.407170123206947));
#38369=CARTESIAN_POINT('Ctrl Pts',(-0.19839786099702,-0.0217051901949521,
0.418288765190064));
#38370=CARTESIAN_POINT('Ctrl Pts',(-0.0892864584974339,-0.178495811879663,
0.429407407173179));
#38371=CARTESIAN_POINT('Ctrl Pts',(0.101615213578872,-0.171776526041577,
0.440526049156296));
#38372=CARTESIAN_POINT('Ctrl Pts',(0.199432941554622,-0.00770249001709277,
0.451644691139412));
#38373=CARTESIAN_POINT('Ctrl Pts',(0.114561442891388,0.16342736102696,0.462763333122529));
#38374=CARTESIAN_POINT('Ctrl Pts',(-0.0752533075803338,0.184850659257176,
0.473881975105645));
#38375=CARTESIAN_POINT('Ctrl Pts',(-0.196132763527948,0.0369427340688636,
0.485000617088761));
#38376=CARTESIAN_POINT('Ctrl Pts',(-0.13734609908354,-0.144806338245697,
0.496119259071877));
#38377=CARTESIAN_POINT('Ctrl Pts',(0.0472555507281729,-0.19390652246629,
0.507237901054994));
#38378=CARTESIAN_POINT('Ctrl Pts',(0.188569065943703,-0.0653799196903168,
0.51835654303811));
#38379=CARTESIAN_POINT('Ctrl Pts',(0.157145135896933,0.123037525956625,
0.529475185021226));
#38380=CARTESIAN_POINT('Ctrl Pts',(-0.0182305561972616,0.198747259981946,
0.540593827004342));
#38381=CARTESIAN_POINT('Ctrl Pts',(-0.176906267902489,0.0923958814363803,
0.551712468987459));
#38382=CARTESIAN_POINT('Ctrl Pts',(-0.173528163328608,-0.0985941329968107,
0.562831110970574));
#38383=CARTESIAN_POINT('Ctrl Pts',(-0.0111907328205795,-0.199267644208816,
0.573949752953692));
#38384=CARTESIAN_POINT('Ctrl Pts',(0.161397894448518,-0.117403348321834,
0.585068394936807));
#38385=CARTESIAN_POINT('Ctrl Pts',(0.186139048335769,0.0720075080408093,
0.596187036919923));
#38386=CARTESIAN_POINT('Ctrl Pts',(0.0403687585131819,0.19545636307293,
0.60730567890304));
#38387=CARTESIAN_POINT('Ctrl Pts',(-0.142381065460884,0.139858709874703,
0.618424320886156));
#38388=CARTESIAN_POINT('Ctrl Pts',(-0.194703656429618,-0.0438555891823412,
0.629542962869273));
#38389=CARTESIAN_POINT('Ctrl Pts',(-0.0686692511086116,-0.187396265922711,
0.640661604852388));
#38390=CARTESIAN_POINT('Ctrl Pts',(0.120269167366484,-0.159273833100625,
0.651780246835506));
#38391=CARTESIAN_POINT('Ctrl Pts',(0.199035810790665,0.0147503407586138,
0.662898888818621));
#38392=CARTESIAN_POINT('Ctrl Pts',(0.0954770165847204,0.175262562555938,
0.674017530801738));
#38393=CARTESIAN_POINT('Ctrl Pts',(-0.09554286697633,0.17522667348191,0.685136172784854));
#38394=CARTESIAN_POINT('Ctrl Pts',(-0.199041339366714,0.0146755494853507,
0.69625481476797));
#38395=CARTESIAN_POINT('Ctrl Pts',(-0.120209309711463,-0.159319014522084,
0.707373456751086));
#38396=CARTESIAN_POINT('Ctrl Pts',(0.0687396627858533,-0.187370449350155,
0.718492098734203));
#38397=CARTESIAN_POINT('Ctrl Pts',(0.194720121977979,-0.0437824237162718,
0.729610740717318));
#38398=CARTESIAN_POINT('Ctrl Pts',(0.142328501723757,0.139912201493195,
0.740729382700435));
#38399=CARTESIAN_POINT('Ctrl Pts',(-0.0404422008722263,0.195441180200575,
0.751848024683551));
#38400=CARTESIAN_POINT('Ctrl Pts',(-0.186166092929526,0.0719375588474842,
0.762966666666667));
#38401=CARTESIAN_POINT('Ctrl Pts',(-0.161353767256008,-0.117463987340584,
0.774085308649784));
#38402=CARTESIAN_POINT('Ctrl Pts',(0.0112656093769942,-0.199263425080664,
0.7852039506329));
#38403=CARTESIAN_POINT('Ctrl Pts',(0.173565199074082,-0.0985289206269375,
0.796322592616017));
#38404=CARTESIAN_POINT('Ctrl Pts',(0.176871536488809,0.0924623496894334,
0.807441234599133));
#38405=CARTESIAN_POINT('Ctrl Pts',(0.0181558731034875,0.198754096312013,
0.818559876582249));
#38406=CARTESIAN_POINT('Ctrl Pts',(-0.157191357711808,0.122978467993954,
0.829678518565365));
#38407=CARTESIAN_POINT('Ctrl Pts',(-0.188544485301595,-0.06545077229961,
0.840797160548482));
#38408=CARTESIAN_POINT('Ctrl Pts',(-0.0471826845453332,-0.193924265639472,
0.851915802531597));
#38409=CARTESIAN_POINT('Ctrl Pts',(0.137400502187529,-0.144754718502077,
0.863034444514714));
#38410=CARTESIAN_POINT('Ctrl Pts',(0.196118868016023,0.0370164308726493,
0.87415308649783));
#38411=CARTESIAN_POINT('Ctrl Pts',(0.0751838422178375,0.184878923522181,
0.885271728480947));
#38412=CARTESIAN_POINT('Ctrl Pts',(-0.114622844578058,0.163384301706618,
0.896390370464062));
#38413=CARTESIAN_POINT('Ctrl Pts',(-0.199430033414812,-0.0077774291863319,
0.90750901244718));
#38414=CARTESIAN_POINT('Ctrl Pts',(-0.101550658722561,-0.171814696636568,
0.918627654430294));
#38415=CARTESIAN_POINT('Ctrl Pts',(0.0893535233606871,-0.178462249679383,
0.929746296413413));
#38416=CARTESIAN_POINT('Ctrl Pts',(0.198406004704164,-0.0216306363946107,
0.940864938396527));
#38417=CARTESIAN_POINT('Ctrl Pts',(0.12570997209806,0.155015572087487,0.951983580379645));
#38418=CARTESIAN_POINT('Ctrl Pts',(-0.0621418372793996,0.18966080308943,
0.963102222362759));
#38419=CARTESIAN_POINT('Ctrl Pts',(-0.193069049565776,0.050568487910749,
0.974220864345877));
#38420=CARTESIAN_POINT('Ctrl Pts',(-0.147136594843111,-0.134846713542859,
0.985339506328992));
#38421=CARTESIAN_POINT('Ctrl Pts',(0.0335792850651442,-0.196736556142493,
0.99645814831211));
#38422=CARTESIAN_POINT('Ctrl Pts',(0.183535233538869,-0.0784070240605622,
1.00757679029522));
#38423=CARTESIAN_POINT('Ctrl Pts',(0.165364659137136,0.111746450372967,
1.01869543227834));
#38424=CARTESIAN_POINT('Ctrl Pts',(-0.00428657180698079,0.199535886614283,
1.02981407426146));
#38425=CARTESIAN_POINT('Ctrl Pts',(-0.170012155281541,0.104540731136874,
1.04093271624457));
#38426=CARTESIAN_POINT('Ctrl Pts',(-0.179997252133044,-0.0862162458906591,
1.05205135822769));
#38427=CARTESIAN_POINT('Ctrl Pts',(-0.0251008199743871,-0.197999253599851,
1.06317000021081));
#38428=CARTESIAN_POINT('Ctrl Pts',(0.152796215902707,-0.128399021223231,
1.07428864219392));
#38429=CARTESIAN_POINT('Ctrl Pts',(0.190711651044001,0.0588063231359589,
1.08540728417704));
#38430=CARTESIAN_POINT('Ctrl Pts',(0.0539529066393858,0.192169106390877,
1.09652592616015));
#38431=CARTESIAN_POINT('Ctrl Pts',(-0.132278503412967,0.149446025304978,
1.10764456814327));
#38432=CARTESIAN_POINT('Ctrl Pts',(-0.197242652143987,-0.0300795429882017,
1.11876321012639));
#38433=CARTESIAN_POINT('Ctrl Pts',(-0.0817058724297523,-0.182236293883171,
1.12988185210951));
#38434=CARTESIAN_POINT('Ctrl Pts',(0.109041866382002,-0.167090592797485,
1.14100049409262));
#38435=CARTESIAN_POINT('Ctrl Pts',(0.169055718360052,-0.0554926552610627,
1.14841292208137));
#38436=CARTESIAN_POINT('Ctrl Pts',(0.16883199391646,0.000672513670271936,
1.15211913607574));
#38437=CARTESIAN_POINT('Ctrl Pts',(-0.0802959149489932,0.163459616787394,
-0.00766913607573554));
#38438=CARTESIAN_POINT('Ctrl Pts',(-0.134673860605774,0.136747655843322,
-0.00396292208136346));
#38439=CARTESIAN_POINT('Ctrl Pts',(-0.213734155664247,0.0252529773779836,
0.00344950590738073));
#38440=CARTESIAN_POINT('Ctrl Pts',(-0.136915832429422,-0.166322257224481,
0.014568147890497));
#38441=CARTESIAN_POINT('Ctrl Pts',(0.0655021664869751,-0.205011034068591,
0.0256867898736133));
#38442=CARTESIAN_POINT('Ctrl Pts',(0.20782545237117,-0.0561654367873057,
0.0368054318567295));
#38443=CARTESIAN_POINT('Ctrl Pts',(0.159819640148463,0.144267659192936,
0.0479240738398458));
#38444=CARTESIAN_POINT('Ctrl Pts',(-0.0346130996849898,0.212473254047885,
0.0590427158229621));
#38445=CARTESIAN_POINT('Ctrl Pts',(-0.197325502634714,0.0860819657174806,
0.0701613578060782));
#38446=CARTESIAN_POINT('Ctrl Pts',(-0.179286136672128,-0.119184009808233,
0.0812799997891947));
#38447=CARTESIAN_POINT('Ctrl Pts',(0.00299076046828686,-0.215261823504807,
0.0923986417723108));
#38448=CARTESIAN_POINT('Ctrl Pts',(0.182526073013706,-0.114155950949091,
0.103517283755427));
#38449=CARTESIAN_POINT('Ctrl Pts',(0.194860591616173,0.0915246053141843,
0.114635925738543));
#38450=CARTESIAN_POINT('Ctrl Pts',(0.0286938251999433,0.213363139543668,
0.12575456772166));
#38451=CARTESIAN_POINT('Ctrl Pts',(-0.163757451921909,0.139752576117334,
0.136873209704776));
#38452=CARTESIAN_POINT('Ctrl Pts',(-0.20619994469249,-0.0618778274775138,
0.147991851687892));
#38453=CARTESIAN_POINT('Ctrl Pts',(-0.0597542656570052,-0.206825237330522,
0.159110493671008));
#38454=CARTESIAN_POINT('Ctrl Pts',(0.141428872795678,-0.162311872087351,
0.170229135654125));
#38455=CARTESIAN_POINT('Ctrl Pts',(0.213057049201279,0.0308862702088754,
0.181347777637241));
#38456=CARTESIAN_POINT('Ctrl Pts',(0.0895157141781652,0.195791217246742,
0.192466419620357));
#38457=CARTESIAN_POINT('Ctrl Pts',(-0.116025892730732,0.181342931797682,
0.203585061603473));
#38458=CARTESIAN_POINT('Ctrl Pts',(-0.215282751312695,0.000776644692787891,
0.21470370358659));
#38459=CARTESIAN_POINT('Ctrl Pts',(-0.1173312682795,-0.180501078038335,
0.225822345569706));
#38460=CARTESIAN_POINT('Ctrl Pts',(0.0881007459369614,-0.196431984868673,
0.236940987552822));
#38461=CARTESIAN_POINT('Ctrl Pts',(0.212828655167567,-0.0324226703065412,
0.248059629535939));
#38462=CARTESIAN_POINT('Ctrl Pts',(0.142596282698117,0.16128721621003,0.259178271519055));
#38463=CARTESIAN_POINT('Ctrl Pts',(-0.0582604709802392,0.207251015763547,
0.270296913502171));
#38464=CARTESIAN_POINT('Ctrl Pts',(-0.205748105739819,0.0633638933400953,
0.281415555485287));
#38465=CARTESIAN_POINT('Ctrl Pts',(-0.16476154945659,-0.138567304257714,
0.292534197468403));
#38466=CARTESIAN_POINT('Ctrl Pts',(0.0271537341065049,-0.213564839618882,
0.30365283945152));
#38467=CARTESIAN_POINT('Ctrl Pts',(0.19419501920302,-0.092927716590924,
0.314771481434636));
#38468=CARTESIAN_POINT('Ctrl Pts',(0.183345241771109,0.11283522638527,0.325890123417753));
#38469=CARTESIAN_POINT('Ctrl Pts',(0.0045432686513366,0.215236206769919,
0.337008765400868));
#38470=CARTESIAN_POINT('Ctrl Pts',(-0.178420535659039,0.120471483967528,
0.348127407383985));
#38471=CARTESIAN_POINT('Ctrl Pts',(-0.197943388729784,-0.08465034466758,
0.359246049367101));
#38472=CARTESIAN_POINT('Ctrl Pts',(-0.0361415101720502,-0.212228785127794,
0.370364691350217));
#38473=CARTESIAN_POINT('Ctrl Pts',(0.158767559662444,-0.145396451102085,
0.381483333333334));
#38474=CARTESIAN_POINT('Ctrl Pts',(0.208238656893164,0.0546253399951339,
0.39260197531645));
#38475=CARTESIAN_POINT('Ctrl Pts',(0.0669541102087431,0.204607949797729,
0.403720617299566));
#38476=CARTESIAN_POINT('Ctrl Pts',(-0.135663306156047,0.167160800898631,
0.414839259282683));
#38477=CARTESIAN_POINT('Ctrl Pts',(-0.214007248481188,-0.0234128937078206,
0.425957901265799));
#38478=CARTESIAN_POINT('Ctrl Pts',(-0.0963112667326238,-0.192539361935742,
0.437076543248915));
#38479=CARTESIAN_POINT('Ctrl Pts',(0.109610013699538,-0.185291421525797,
0.448195185232032));
#38480=CARTESIAN_POINT('Ctrl Pts',(0.215123766275159,-0.00830850033729405,
0.459313827215147));
#38481=CARTESIAN_POINT('Ctrl Pts',(0.123574816038915,0.176285367615161,
0.470432469198265));
#38482=CARTESIAN_POINT('Ctrl Pts',(-0.0811740268440561,0.199394190888763,
0.48155111118138));
#38483=CARTESIAN_POINT('Ctrl Pts',(-0.211563939493572,0.0398492848144611,
0.492669753164497));
#38484=CARTESIAN_POINT('Ctrl Pts',(-0.148152105102257,-0.156199294966507,
0.503788395147612));
#38485=CARTESIAN_POINT('Ctrl Pts',(0.0509734849759847,-0.20916254402657,
0.51490703713073));
#38486=CARTESIAN_POINT('Ctrl Pts',(0.203405151388631,-0.0705238284754304,
0.526025679113844));
#38487=CARTESIAN_POINT('Ctrl Pts',(0.169508874624462,0.132717773556567,
0.537144321096963));
#38488=CARTESIAN_POINT('Ctrl Pts',(-0.019664885248515,0.21438413719869,
0.548262963080077));
#38489=CARTESIAN_POINT('Ctrl Pts',(-0.190824757094816,0.0996653303509719,
0.559381605063195));
#38490=CARTESIAN_POINT('Ctrl Pts',(-0.187180872723762,-0.106351242967042,
0.570500247046309));
#38491=CARTESIAN_POINT('Ctrl Pts',(-0.012071188305083,-0.214945463797604,
0.581618889029427));
#38492=CARTESIAN_POINT('Ctrl Pts',(0.174096228296046,-0.126640314621194,
0.592737531012542));
#38493=CARTESIAN_POINT('Ctrl Pts',(0.200783946807991,0.0776728568965356,
0.60385617299566));
#38494=CARTESIAN_POINT('Ctrl Pts',(0.0435448592570146,0.210834321747079,
0.614974814978775));
#38495=CARTESIAN_POINT('Ctrl Pts',(-0.153583208518367,0.150862401066228,
0.626093456961893));
#38496=CARTESIAN_POINT('Ctrl Pts',(-0.210022394255324,-0.0473060239877022,
0.637212098945007));
#38497=CARTESIAN_POINT('Ctrl Pts',(-0.074071955267899,-0.202140078749996,
0.648330740928124));
#38498=CARTESIAN_POINT('Ctrl Pts',(0.129731608273796,-0.171805051756223,
0.65944938291124));
#38499=CARTESIAN_POINT('Ctrl Pts',(0.214695390376071,0.015910856216126,
0.670568024894357));
#38500=CARTESIAN_POINT('Ctrl Pts',(0.102988880574655,0.189051729619815,
0.681686666877473));
#38501=CARTESIAN_POINT('Ctrl Pts',(-0.103059911890458,0.189013016894061,
0.692805308860589));
#38502=CARTESIAN_POINT('Ctrl Pts',(-0.214701353924984,0.0158301805751674,
0.703923950843705));
#38503=CARTESIAN_POINT('Ctrl Pts',(-0.129667041186295,-0.171853787925252,
0.715042592826822));
#38504=CARTESIAN_POINT('Ctrl Pts',(0.0741479067384996,-0.20211223100189,
0.726161234809938));
#38505=CARTESIAN_POINT('Ctrl Pts',(0.210040155266868,-0.0472271020678894,
0.737279876793055));
#38506=CARTESIAN_POINT('Ctrl Pts',(0.153526509213771,0.150920101255294,
0.748398518776171));
#38507=CARTESIAN_POINT('Ctrl Pts',(-0.0436240798549652,0.210817944328893,
0.759517160759286));
#38508=CARTESIAN_POINT('Ctrl Pts',(-0.200813119194563,0.0775974042967894,
0.770635802742404));
#38509=CARTESIAN_POINT('Ctrl Pts',(-0.174048629299744,-0.126705724547931,
0.781754444725519));
#38510=CARTESIAN_POINT('Ctrl Pts',(0.0121519559390324,-0.214940912720278,
0.792873086708636));
#38511=CARTESIAN_POINT('Ctrl Pts',(0.187220822337856,-0.106280899870737,
0.803991728691751));
#38512=CARTESIAN_POINT('Ctrl Pts',(0.190787293110882,0.0997370281398245,
0.815110370674869));
#38513=CARTESIAN_POINT('Ctrl Pts',(0.0195843262983046,0.21439151139204,
0.826229012657984));
#38514=CARTESIAN_POINT('Ctrl Pts',(-0.169558733042143,0.132654069078969,
0.837347654641101));
#38515=CARTESIAN_POINT('Ctrl Pts',(-0.203378636810517,-0.0706002555693802,
0.848466296624217));
#38516=CARTESIAN_POINT('Ctrl Pts',(-0.0508948858861673,-0.209181683182873,
0.859584938607333));
#38517=CARTESIAN_POINT('Ctrl Pts',(0.148210788489943,-0.156143613926181,
0.870703580590451));
#38518=CARTESIAN_POINT('Ctrl Pts',(0.211548950721726,0.0399287798761521,
0.881822222573564));
#38519=CARTESIAN_POINT('Ctrl Pts',(0.0810990961415922,0.199424678906897,
0.892940864556684));
#38520=CARTESIAN_POINT('Ctrl Pts',(-0.123641048638147,0.176238920508216,
0.904059506539796));
#38521=CARTESIAN_POINT('Ctrl Pts',(-0.215120629331062,-0.00838933551026959,
0.915178148522916));
#38522=CARTESIAN_POINT('Ctrl Pts',(-0.109540379848118,-0.185332595276186,
0.926296790506031));
#38523=CARTESIAN_POINT('Ctrl Pts',(0.0963836080712942,-0.19250315915564,
0.937415432489146));
#38524=CARTESIAN_POINT('Ctrl Pts',(0.214016032912378,-0.0233324742234878,
0.948534074472264));
#38525=CARTESIAN_POINT('Ctrl Pts',(0.135600480268067,0.167211762704833,
0.95965271645538));
#38526=CARTESIAN_POINT('Ctrl Pts',(-0.0670309828185569,0.204582783352242,
0.970771358438496));
#38527=CARTESIAN_POINT('Ctrl Pts',(-0.208259181106143,0.0545470747680921,
0.981890000421612));
#38528=CARTESIAN_POINT('Ctrl Pts',(-0.158712889620009,-0.145456074914393,
0.993008642404728));
#38529=CARTESIAN_POINT('Ctrl Pts',(0.0362212090727357,-0.212215236818265,
1.00412728438785));
#38530=CARTESIAN_POINT('Ctrl Pts',(0.197975271162805,-0.0845758688953388,
1.01524592637096));
#38531=CARTESIAN_POINT('Ctrl Pts',(0.178375086909329,0.120538347801125,
1.02636456835408));
#38532=CARTESIAN_POINT('Ctrl Pts',(-0.00462382725911752,0.215234810763501,
1.03748321033719));
#38533=CARTESIAN_POINT('Ctrl Pts',(-0.183388235020868,0.112765702777161,
1.04860185232031));
#38534=CARTESIAN_POINT('Ctrl Pts',(-0.194158931298892,-0.0929994984054507,
1.05972049430343));
#38535=CARTESIAN_POINT('Ctrl Pts',(-0.0270756821184746,-0.213577279771527,
1.07083913628654));
#38536=CARTESIAN_POINT('Ctrl Pts',(0.164817793797518,-0.138501096239512,
1.08195777826966));
#38537=CARTESIAN_POINT('Ctrl Pts',(0.20571630907777,0.0634330397736036,
1.09307642025277));
#38538=CARTESIAN_POINT('Ctrl Pts',(0.058197770073898,0.207288432925282,
1.10419506223589));
#38539=CARTESIAN_POINT('Ctrl Pts',(-0.142685805211597,0.161204019596003,
1.11531370421901));
#38540=CARTESIAN_POINT('Ctrl Pts',(-0.212761151034289,-0.0324461171008946,
1.12643234620212));
#38541=CARTESIAN_POINT('Ctrl Pts',(-0.0881342614057178,-0.196574134576644,
1.13755098818524));
#38542=CARTESIAN_POINT('Ctrl Pts',(0.117620974724197,-0.180236812191326,
1.14866963016836));
#38543=CARTESIAN_POINT('Ctrl Pts',(0.182356548323819,-0.0598586618003602,
1.1560820581571));
#38544=CARTESIAN_POINT('Ctrl Pts',(0.182115221868229,0.000725425160419088,
1.15978827215147));
#38545=CARTESIAN_POINT('Ctrl Pts',(-0.0861525859670525,0.175382131162755,
-1.38777878078145E-17));
#38546=CARTESIAN_POINT('Ctrl Pts',(-0.144496782441849,0.146721837385112,
0.00370621399437207));
#38547=CARTESIAN_POINT('Ctrl Pts',(-0.229323624142731,0.0270948940037977,
0.0111186419831162));
#38548=CARTESIAN_POINT('Ctrl Pts',(-0.14690228053469,-0.178453568564088,
0.0222372839662325));
#38549=CARTESIAN_POINT('Ctrl Pts',(0.0702798023147504,-0.219964250335881,
0.0333559259493488));
#38550=CARTESIAN_POINT('Ctrl Pts',(0.222983948348091,-0.0602620646924488,
0.044474567932465));
#38551=CARTESIAN_POINT('Ctrl Pts',(0.171476659751129,0.154790339194469,
0.0555932099155814));
#38552=CARTESIAN_POINT('Ctrl Pts',(-0.0371377304572895,0.22797075413722,
0.0667118518986976));
#38553=CARTESIAN_POINT('Ctrl Pts',(-0.211718147056775,0.0923606631345987,
0.0778304938818138));
#38554=CARTESIAN_POINT('Ctrl Pts',(-0.192363015131696,-0.12787712372945,
0.0889491358649302));
#38555=CARTESIAN_POINT('Ctrl Pts',(0.00320890232727887,-0.230962717925356,
0.100067777848046));
#38556=CARTESIAN_POINT('Ctrl Pts',(0.195839267869742,-0.122482325334233,
0.111186419831163));
#38557=CARTESIAN_POINT('Ctrl Pts',(0.209073448897961,0.0982002812028443,
0.122305061814279));
#38558=CARTESIAN_POINT('Ctrl Pts',(0.0307867124228199,0.228925546628532,
0.133423703797395));
#38559=CARTESIAN_POINT('Ctrl Pts',(-0.175701689972769,0.149945932314417,
0.144542345780511));
#38560=CARTESIAN_POINT('Ctrl Pts',(-0.221239878427269,-0.0663911091192784,
0.155660987763628));
#38561=CARTESIAN_POINT('Ctrl Pts',(-0.0641126576885465,-0.221910779030204,
0.166779629746744));
#38562=CARTESIAN_POINT('Ctrl Pts',(0.151744495713052,-0.174150671579767,
0.17789827172986));
#38563=CARTESIAN_POINT('Ctrl Pts',(0.228597130487397,0.0331390712847842,
0.189016913712977));
#38564=CARTESIAN_POINT('Ctrl Pts',(0.0960448643749269,0.210071953052146,
0.200135555696093));
#38565=CARTESIAN_POINT('Ctrl Pts',(-0.124488658037438,0.194569829998722,
0.211254197679209));
#38566=CARTESIAN_POINT('Ctrl Pts',(-0.230985172178094,0.000833292063536468,
0.222372839662325));
#38567=CARTESIAN_POINT('Ctrl Pts',(-0.12588924584139,-0.193666572611094,
0.233491481645442));
#38568=CARTESIAN_POINT('Ctrl Pts',(0.0945266903418065,-0.210759457362527,
0.244610123628558));
#38569=CARTESIAN_POINT('Ctrl Pts',(0.228352077714336,-0.0347875342430591,
0.255728765611674));
#38570=CARTESIAN_POINT('Ctrl Pts',(0.152997054850621,0.173051278744978,
0.26684740759479));
#38571=CARTESIAN_POINT('Ctrl Pts',(-0.0625099077306038,0.222367613142842,
0.277966049577907));
#38572=CARTESIAN_POINT('Ctrl Pts',(-0.220755082977362,0.0679855665342084,
0.289084691561023));
#38573=CARTESIAN_POINT('Ctrl Pts',(-0.176779024968342,-0.148674208393651,
0.300203333544139));
#38574=CARTESIAN_POINT('Ctrl Pts',(0.0291342892527361,-0.229141958423335,
0.311321975527256));
#38575=CARTESIAN_POINT('Ctrl Pts',(0.208359330569799,-0.0997057334412016,
0.322440617510372));
#38576=CARTESIAN_POINT('Ctrl Pts',(0.196718185643314,0.121065268979674,
0.333559259493488));
#38577=CARTESIAN_POINT('Ctrl Pts',(0.00487464827201324,0.230935232741881,
0.344677901476604));
#38578=CARTESIAN_POINT('Ctrl Pts',(-0.191434278399063,0.129258504441778,
0.355796543459721));
#38579=CARTESIAN_POINT('Ctrl Pts',(-0.212381100893932,-0.0908246216603541,
0.366915185442837));
#38580=CARTESIAN_POINT('Ctrl Pts',(-0.038777621054007,-0.227708453998192,
0.378033827425954));
#38581=CARTESIAN_POINT('Ctrl Pts',(0.170347841995286,-0.156001463596674,
0.389152469409069));
#38582=CARTESIAN_POINT('Ctrl Pts',(0.223427291426326,0.058609635407974,
0.400271111392186));
#38583=CARTESIAN_POINT('Ctrl Pts',(0.0718376487679439,0.219531765665651,
0.411389753375301));
#38584=CARTESIAN_POINT('Ctrl Pts',(-0.145558396757891,0.179353274433565,
0.422508395358419));
#38585=CARTESIAN_POINT('Ctrl Pts',(-0.229616635965357,-0.0251205972206891,
0.433627037341534));
#38586=CARTESIAN_POINT('Ctrl Pts',(-0.103336074967814,-0.206582911991821,
0.444745679324651));
#38587=CARTESIAN_POINT('Ctrl Pts',(0.117604813820203,-0.198806317010017,
0.455864321307767));
#38588=CARTESIAN_POINT('Ctrl Pts',(0.230814590995695,-0.00891451065749571,
0.466982963290884));
#38589=CARTESIAN_POINT('Ctrl Pts',(0.132588189186442,0.189143374203362,
0.478101605273999));
#38590=CARTESIAN_POINT('Ctrl Pts',(-0.0870947461077786,0.21393772252035,
0.489220247257116));
#38591=CARTESIAN_POINT('Ctrl Pts',(-0.226995115459196,0.0427558355600586,
0.500338889240232));
#38592=CARTESIAN_POINT('Ctrl Pts',(-0.158958111120973,-0.167592251687317,
0.511457531223348));
#38593=CARTESIAN_POINT('Ctrl Pts',(0.0546914192237968,-0.224418565586851,
0.522576173206465));
#38594=CARTESIAN_POINT('Ctrl Pts',(0.21824123683356,-0.0756677372605439,
0.533694815189581));
#38595=CARTESIAN_POINT('Ctrl Pts',(0.181872613351991,0.14239802115651,0.544813457172697));
#38596=CARTESIAN_POINT('Ctrl Pts',(-0.0210992142997687,0.230021014415434,
0.555932099155813));
#38597=CARTESIAN_POINT('Ctrl Pts',(-0.204743246287144,0.106934779265563,
0.567050741138931));
#38598=CARTESIAN_POINT('Ctrl Pts',(-0.200833582118916,-0.114108352937273,
0.578169383122044));
#38599=CARTESIAN_POINT('Ctrl Pts',(-0.0129516437895867,-0.230623283386393,
0.589288025105164));
#38600=CARTESIAN_POINT('Ctrl Pts',(0.186794562143574,-0.135877280920554,
0.600406667088277));
#38601=CARTESIAN_POINT('Ctrl Pts',(0.215428845280213,0.083338205752262,
0.611525309071395));
#38602=CARTESIAN_POINT('Ctrl Pts',(0.0467209600008474,0.226212280421227,
0.622643951054511));
#38603=CARTESIAN_POINT('Ctrl Pts',(-0.164785351575852,0.161866092257753,
0.633762593037627));
#38604=CARTESIAN_POINT('Ctrl Pts',(-0.225341132081031,-0.0507564587930634,
0.644881235020743));
#38605=CARTESIAN_POINT('Ctrl Pts',(-0.0794746594271866,-0.21688389157728,
0.655999877003859));
#38606=CARTESIAN_POINT('Ctrl Pts',(0.139194049181108,-0.184336270411821,
0.667118518986976));
#38607=CARTESIAN_POINT('Ctrl Pts',(0.230354969961477,0.0170713716736379,
0.678237160970093));
#38608=CARTESIAN_POINT('Ctrl Pts',(0.11050074456459,0.202840896683692,0.689355802953208));
#38609=CARTESIAN_POINT('Ctrl Pts',(-0.110576956804586,0.202799360306213,
0.700474444936325));
#38610=CARTESIAN_POINT('Ctrl Pts',(-0.230361368483253,0.0169848116649841,
0.711593086919441));
#38611=CARTESIAN_POINT('Ctrl Pts',(-0.139124772661127,-0.184388561328419,
0.722711728902557));
#38612=CARTESIAN_POINT('Ctrl Pts',(0.0795561506911461,-0.216854012653626,
0.733830370885674));
#38613=CARTESIAN_POINT('Ctrl Pts',(0.225360188555757,-0.0506717804195071,
0.744949012868789));
#38614=CARTESIAN_POINT('Ctrl Pts',(0.164724516703786,0.161928001017393,
0.756067654851907));
#38615=CARTESIAN_POINT('Ctrl Pts',(-0.0468059588377044,0.226194708457211,
0.767186296835021));
#38616=CARTESIAN_POINT('Ctrl Pts',(-0.2154601454596,0.0832572497460946,
0.778304938818139));
#38617=CARTESIAN_POINT('Ctrl Pts',(-0.18674349134348,-0.135947461755279,
0.789423580801255));
#38618=CARTESIAN_POINT('Ctrl Pts',(0.0130383025010703,-0.230618400359892,
0.800542222784371));
#38619=CARTESIAN_POINT('Ctrl Pts',(0.200876445601631,-0.114032879114536,
0.811660864767487));
#38620=CARTESIAN_POINT('Ctrl Pts',(0.204703049732954,0.107011706590215,
0.822779506750604));
#38621=CARTESIAN_POINT('Ctrl Pts',(0.0210127794931219,0.230028926472067,
0.83389814873372));
#38622=CARTESIAN_POINT('Ctrl Pts',(-0.181926108372479,0.142329670163983,
0.845016790716836));
#38623=CARTESIAN_POINT('Ctrl Pts',(-0.218212788319439,-0.0757497388391501,
0.856135432699953));
#38624=CARTESIAN_POINT('Ctrl Pts',(-0.0546070872270015,-0.224439100726275,
0.867254074683069));
#38625=CARTESIAN_POINT('Ctrl Pts',(0.159021074792356,-0.167532509350284,
0.878372716666185));
#38626=CARTESIAN_POINT('Ctrl Pts',(0.226979033427429,0.0428411288796547,
0.889491358649301));
#38627=CARTESIAN_POINT('Ctrl Pts',(0.0870143500653468,0.213970434291613,
0.900610000632417));
#38628=CARTESIAN_POINT('Ctrl Pts',(-0.132659252698235,0.189093539309814,
0.911728642615534));
#38629=CARTESIAN_POINT('Ctrl Pts',(-0.230811225247311,-0.00900124183420705,
0.92284728459865));
#38630=CARTESIAN_POINT('Ctrl Pts',(-0.117530100973675,-0.198850493915805,
0.933965926581767));
#38631=CARTESIAN_POINT('Ctrl Pts',(0.103413692781901,-0.206544068631896,
0.945084568564882));
#38632=CARTESIAN_POINT('Ctrl Pts',(0.229626061120593,-0.0250343120523647,
0.956203210547999));
#38633=CARTESIAN_POINT('Ctrl Pts',(0.145490988438074,0.179407953322179,
0.967321852531115));
#38634=CARTESIAN_POINT('Ctrl Pts',(-0.0719201283577143,0.219504763615053,
0.978440494514231));
#38635=CARTESIAN_POINT('Ctrl Pts',(-0.22344931264651,0.0585256616254353,
0.989559136497349));
#38636=CARTESIAN_POINT('Ctrl Pts',(-0.170289184396906,-0.156065436285928,
1.00067777848046));
#38637=CARTESIAN_POINT('Ctrl Pts',(0.0388631330803271,-0.227693917494037,
1.01179642046358));
#38638=CARTESIAN_POINT('Ctrl Pts',(0.21241530878674,-0.0907447137301155,
1.0229150624467));
#38639=CARTESIAN_POINT('Ctrl Pts',(0.191385514681521,0.129330245229283,
1.03403370442981));
#38640=CARTESIAN_POINT('Ctrl Pts',(-0.00496108271125438,0.230933734912719,
1.04515234641293));
#38641=CARTESIAN_POINT('Ctrl Pts',(-0.196764314760194,0.120990674417448,
1.05627098839605));
#38642=CARTESIAN_POINT('Ctrl Pts',(-0.208320610464741,-0.0997827509202423,
1.06738963037916));
#38643=CARTESIAN_POINT('Ctrl Pts',(-0.0290505442625618,-0.229155305943203,
1.07850827236228));
#38644=CARTESIAN_POINT('Ctrl Pts',(0.17683937169233,-0.148603171255794,
1.08962691434539));
#38645=CARTESIAN_POINT('Ctrl Pts',(0.220720967111538,0.0680597564112484,
1.10074555632851));
#38646=CARTESIAN_POINT('Ctrl Pts',(0.0624426335084105,0.222407759459687,
1.11186419831163));
#38647=CARTESIAN_POINT('Ctrl Pts',(-0.153093107010227,0.172962013887028,
1.12298284029474));
#38648=CARTESIAN_POINT('Ctrl Pts',(-0.228279649924591,-0.0348126912135875,
1.13410148227786));
#38649=CARTESIAN_POINT('Ctrl Pts',(-0.0945626503816835,-0.210911975270116,
1.14522012426097));
#38650=CARTESIAN_POINT('Ctrl Pts',(0.126200083066393,-0.193383031585166,
1.15633876624409));
#38651=CARTESIAN_POINT('Ctrl Pts',(0.195657378287586,-0.0642246683396576,
1.16375119423284));
#38652=CARTESIAN_POINT('Ctrl Pts',(0.195398449819998,0.00077833665056624,
1.16745740822721));
#38653=CARTESIAN_POINT('Ctrl Pts',(-0.195093054978418,-5.50606481354719E-5,
1.06241303078758));
#38654=CARTESIAN_POINT('Ctrl Pts',(-0.195166977968097,-0.0292567552961119,
1.0640718973181));
#38655=CARTESIAN_POINT('Ctrl Pts',(-0.189027401228485,-0.0584289311968449,
1.06573076384863));
#38656=CARTESIAN_POINT('Ctrl Pts',(-0.17651621681362,-0.0845492725344543,
1.06738963037916));
#38657=CARTESIAN_POINT('Ctrl Pts',(-0.148563921730681,-0.142906935927896,
1.07109584437353));
#38658=CARTESIAN_POINT('Ctrl Pts',(-0.0888072329966215,-0.18603112093555,
1.07480205836791));
#38659=CARTESIAN_POINT('Ctrl Pts',(-0.0246139026371096,-0.194167857658142,
1.07850827236228));
#38660=CARTESIAN_POINT('Ctrl Pts',(0.0395794277224022,-0.202304594380734,
1.08221448635665));
#38661=CARTESIAN_POINT('Ctrl Pts',(0.108209399707366,-0.175453882818264,
1.08592070035102));
#38662=CARTESIAN_POINT('Ctrl Pts',(0.149837984936383,-0.125918039092522,
1.08962691434539));
#38663=CARTESIAN_POINT('Ctrl Pts',(0.191466570165399,-0.0763821953667804,
1.09333312833977));
#38664=CARTESIAN_POINT('Ctrl Pts',(0.206093768638468,-0.0041612194777677,
1.09703934233414));
#38665=CARTESIAN_POINT('Ctrl Pts',(0.187027645607817,0.0576739356414784,
1.10074555632851));
#38666=CARTESIAN_POINT('Ctrl Pts',(0.180418088670294,0.0791100177355746,
1.10203037088567));
#38667=CARTESIAN_POINT('Ctrl Pts',(0.169759382901609,0.0992979671982257,
1.10331518544284));
#38668=CARTESIAN_POINT('Ctrl Pts',(0.156057659382855,0.117255425406022,
1.1046));
#38669=CARTESIAN_POINT('Ctrl Pts',(-0.09055496143049,-0.12679201530598,
5.09575021068187E-18));
#38670=CARTESIAN_POINT('Ctrl Pts',(-0.0937460871048188,-0.125085822491965,
4.58984227758833E-18));
#38671=CARTESIAN_POINT('Ctrl Pts',(-0.0968677330061127,-0.123263760516135,
2.50662287286079E-17));
#38672=CARTESIAN_POINT('Ctrl Pts',(-0.0999128467894991,-0.121327242330634,
2.00577401909818E-17));
#38673=CARTESIAN_POINT('Ctrl Pts',(-0.107335152566795,-0.11660708041271,
6.42545598945985E-18));
#38674=CARTESIAN_POINT('Ctrl Pts',(-0.11430344392066,-0.111208610599775,
9.99023806675092E-18));
#38675=CARTESIAN_POINT('Ctrl Pts',(-0.120790707516777,-0.105232728283189,
2.60208521396521E-17));
#38676=CARTESIAN_POINT('Ctrl Pts',(-0.123891078118351,-0.102376755255687,
3.36821478247169E-17));
#38677=CARTESIAN_POINT('Ctrl Pts',(-0.126881418116351,-0.099388034385428,
-1.92452104322545E-17));
#38678=CARTESIAN_POINT('Ctrl Pts',(-0.129748204847616,-0.0962880923092239,
-1.51788304147971E-17));
#38679=CARTESIAN_POINT('Ctrl Pts',(-0.135037647654988,-0.0905684598931024,
-7.67604539740766E-18));
#38680=CARTESIAN_POINT('Ctrl Pts',(-0.139916189540312,-0.0844627163539483,
6.65058155921973E-18));
#38681=CARTESIAN_POINT('Ctrl Pts',(-0.144364609008094,-0.0780350740853688,
-6.07153216591882E-18));
#38682=CARTESIAN_POINT('Ctrl Pts',(-0.146693883418799,-0.0746694421422029,
-1.2733065360948E-17));
#38683=CARTESIAN_POINT('Ctrl Pts',(-0.148905919766188,-0.0712140221787596,
5.51914947350105E-18));
#38684=CARTESIAN_POINT('Ctrl Pts',(-0.150994732263837,-0.0676811328914676,
3.46944695195361E-18));
#38685=CARTESIAN_POINT('Ctrl Pts',(-0.156930492501974,-0.0576417522477531,
-2.35517480854577E-18));
#38686=CARTESIAN_POINT('Ctrl Pts',(-0.161837586723136,-0.04704232833817,
1.0498384979768E-17));
#38687=CARTESIAN_POINT('Ctrl Pts',(-0.165656700638674,-0.0360824270657778,
6.93889390390723E-18));
#38688=CARTESIAN_POINT('Ctrl Pts',(-0.168566598677898,-0.0277317478433351,
4.22681033390876E-18));
#38689=CARTESIAN_POINT('Ctrl Pts',(-0.17084455406887,-0.0191704748820838,
-1.37633633951559E-17));
#38690=CARTESIAN_POINT('Ctrl Pts',(-0.172449224480544,-0.0104741012692795,
-1.56125112837913E-17));
#38691=CARTESIAN_POINT('Ctrl Pts',(-0.173092222694612,-0.00698942761839798,
-1.63534726558537E-17));
#38692=CARTESIAN_POINT('Ctrl Pts',(-0.173626618765139,-0.00348302750915761,
-1.21488779396688E-17));
#38693=CARTESIAN_POINT('Ctrl Pts',(-0.174048178602262,2.59546856150664E-5,
-1.38777878078145E-17));
#38694=CARTESIAN_POINT('Ctrl Pts',(-0.174866886128293,0.00684071709555691,
-1.72354879401115E-17));
#38695=CARTESIAN_POINT('Ctrl Pts',(-0.175263001859704,0.0136781916586682,
-1.47570089434246E-17));
#38696=CARTESIAN_POINT('Ctrl Pts',(-0.175222496230419,0.020502014676713,
-1.73472347597681E-17));
#38697=CARTESIAN_POINT('Ctrl Pts',(-0.175176789703203,0.0282020123806742,
-2.02700439806174E-17));
#38698=CARTESIAN_POINT('Ctrl Pts',(-0.174575488437737,0.0358847565960055,
-4.14656083691159E-17));
#38699=CARTESIAN_POINT('Ctrl Pts',(-0.173454133268089,0.0435109284941294,
-3.81639164714898E-17));
#38700=CARTESIAN_POINT('Ctrl Pts',(-0.172772227559337,0.0481484691182048,
-3.61561292739328E-17));
#38701=CARTESIAN_POINT('Ctrl Pts',(-0.171897804056446,0.0527651363053484,
-4.88916554017709E-17));
#38702=CARTESIAN_POINT('Ctrl Pts',(-0.170837068741884,0.0573521982187067,
-5.03069808033274E-17));
#38703=CARTESIAN_POINT('Ctrl Pts',(-0.170031029630167,0.0608378475218587,
-5.1382468357856E-17));
#38704=CARTESIAN_POINT('Ctrl Pts',(-0.169117246541092,0.0643057763689402,
-8.52354934901958E-18));
#38705=CARTESIAN_POINT('Ctrl Pts',(-0.168102750715484,0.0677391082731898,
-8.67361737988404E-18));
#38706=CARTESIAN_POINT('Ctrl Pts',(-0.164848133533702,0.0787536247692379,
-9.1550525709997E-18));
#38707=CARTESIAN_POINT('Ctrl Pts',(-0.160552714845615,0.0894467883889295,
-1.4615508474092E-17));
#38708=CARTESIAN_POINT('Ctrl Pts',(-0.155326482610649,0.0996955319262882,
-3.12250225675825E-17));
#38709=CARTESIAN_POINT('Ctrl Pts',(-0.152120282364142,0.105982953261303,
-4.14146631703528E-17));
#38710=CARTESIAN_POINT('Ctrl Pts',(-0.148562901683281,0.112103241720107,
-3.61201279282247E-17));
#38711=CARTESIAN_POINT('Ctrl Pts',(-0.144672442230625,0.118026999364952,
-4.16333634234434E-17));
#38712=CARTESIAN_POINT('Ctrl Pts',(-0.141744976772053,0.122484466690154,
-4.57819239401724E-17));
#38713=CARTESIAN_POINT('Ctrl Pts',(-0.138624730042886,0.126835138052646,
-6.23512024481927E-18));
#38714=CARTESIAN_POINT('Ctrl Pts',(-0.135339728450536,0.131039395408961,
-6.93889390390723E-18));
#38715=CARTESIAN_POINT('Ctrl Pts',(-0.127443588741529,0.141145144987709,
-8.63055065945266E-18));
#38716=CARTESIAN_POINT('Ctrl Pts',(-0.118584883784043,0.150432575075823,
-5.34207396488032E-18));
#38717=CARTESIAN_POINT('Ctrl Pts',(-0.108881311648901,0.158738497602418,
0.));
#38718=CARTESIAN_POINT('Ctrl Pts',(-0.101751737768341,0.16484116654483,
3.92501961933201E-18));
#38719=CARTESIAN_POINT('Ctrl Pts',(-0.0941648935161059,0.170414009123921,
-1.10648570806265E-17));
#38720=CARTESIAN_POINT('Ctrl Pts',(-0.0861525859670525,0.175382131162755,
-1.38777878078145E-17));
#38721=CARTESIAN_POINT('Origin',(0.,0.,0.));
#38722=CARTESIAN_POINT('Origin',(-0.0866025403784439,-0.15,-0.4));
#38723=CARTESIAN_POINT('',(-0.0866025403784439,-0.15,-0.4));
#38724=CARTESIAN_POINT('',(0.0866025403784439,-0.15,-0.4));
#38725=CARTESIAN_POINT('',(-0.043301270189222,-0.15,-0.4));
#38726=CARTESIAN_POINT('',(-0.0866025403784439,-0.15,-0.2));
#38727=CARTESIAN_POINT('',(-0.0866025403784439,-0.15,-0.4));
#38728=CARTESIAN_POINT('',(0.0866025403784439,-0.15,-0.2));
#38729=CARTESIAN_POINT('',(-0.0866025403784439,-0.15,-0.2));
#38730=CARTESIAN_POINT('',(0.0866025403784439,-0.15,-0.4));
#38731=CARTESIAN_POINT('Origin',(-0.173205080756888,2.12115047744981E-17,
-0.4));
#38732=CARTESIAN_POINT('',(-0.173205080756888,2.12115047744981E-17,-0.4));
#38733=CARTESIAN_POINT('',(-0.151554445662277,-0.0375,-0.4));
#38734=CARTESIAN_POINT('',(-0.173205080756888,2.77555756156289E-17,-0.2));
#38735=CARTESIAN_POINT('',(-0.173205080756888,2.12115047744981E-17,-0.4));
#38736=CARTESIAN_POINT('',(-0.173205080756888,2.12115047744981E-17,-0.2));
#38737=CARTESIAN_POINT('Origin',(-0.0866025403784438,0.15,-0.4));
#38738=CARTESIAN_POINT('',(-0.0866025403784438,0.15,-0.4));
#38739=CARTESIAN_POINT('',(-0.108253175473055,0.1125,-0.4));
#38740=CARTESIAN_POINT('',(-0.0866025403784438,0.15,-0.2));
#38741=CARTESIAN_POINT('',(-0.0866025403784438,0.15,-0.4));
#38742=CARTESIAN_POINT('',(-0.0866025403784438,0.15,-0.2));
#38743=CARTESIAN_POINT('Origin',(0.0866025403784439,0.15,-0.4));
#38744=CARTESIAN_POINT('',(0.0866025403784439,0.15,-0.4));
#38745=CARTESIAN_POINT('',(0.043301270189222,0.15,-0.4));
#38746=CARTESIAN_POINT('',(0.0866025403784439,0.15,-0.2));
#38747=CARTESIAN_POINT('',(0.0866025403784439,0.15,-0.4));
#38748=CARTESIAN_POINT('',(0.0866025403784439,0.15,-0.2));
#38749=CARTESIAN_POINT('Origin',(0.173205080756888,0.,-0.4));
#38750=CARTESIAN_POINT('',(0.173205080756888,0.,-0.4));
#38751=CARTESIAN_POINT('',(0.151554445662277,0.0375,-0.4));
#38752=CARTESIAN_POINT('',(0.173205080756888,0.,-0.2));
#38753=CARTESIAN_POINT('',(0.173205080756888,0.,-0.4));
#38754=CARTESIAN_POINT('',(0.173205080756888,0.,-0.2));
#38755=CARTESIAN_POINT('Origin',(0.0866025403784439,-0.15,-0.4));
#38756=CARTESIAN_POINT('',(0.108253175473055,-0.1125,-0.4));
#38757=CARTESIAN_POINT('',(0.0866025403784439,-0.15,-0.2));
#38758=CARTESIAN_POINT('Origin',(0.,2.77555756156289E-17,-0.2));
#38759=CARTESIAN_POINT('Origin',(0.,0.,0.));
#38760=CARTESIAN_POINT('',(-0.35,-4.28626379701574E-17,0.));
#38761=CARTESIAN_POINT('Origin',(0.,0.,0.));
#38762=CARTESIAN_POINT('Origin',(0.,0.,-0.4));
#38763=CARTESIAN_POINT('',(-0.35,-4.28626379701574E-17,-0.4));
#38764=CARTESIAN_POINT('',(-0.35,-4.28626379701574E-17,-0.4));
#38765=CARTESIAN_POINT('Origin',(0.,0.,-0.4));
#38766=CARTESIAN_POINT('Origin',(0.,0.,-0.4));
#38767=CARTESIAN_POINT('Origin',(0.,0.,1.2));
#43957=UNCERTAINTY_MEASURE_WITH_UNIT(LENGTH_MEASURE(0.001),#43981,
'DISTANCE_ACCURACY_VALUE',
'Maximum model space distance between geometric entities at asserted c
onnectivities');
#43961=UNCERTAINTY_MEASURE_WITH_UNIT(LENGTH_MEASURE(0.001),#43981,
'DISTANCE_ACCURACY_VALUE',
'Maximum model space distance between geometric entities at asserted c
onnectivities');
#43976=(
GEOMETRIC_REPRESENTATION_CONTEXT(3)
GLOBAL_UNCERTAINTY_ASSIGNED_CONTEXT((#43957))
GLOBAL_UNIT_ASSIGNED_CONTEXT((#43981,#43983,#43984))
REPRESENTATION_CONTEXT('','3D')
);
#43980=(
GEOMETRIC_REPRESENTATION_CONTEXT(3)
GLOBAL_UNCERTAINTY_ASSIGNED_CONTEXT((#43961))
GLOBAL_UNIT_ASSIGNED_CONTEXT((#43981,#43983,#43984))
REPRESENTATION_CONTEXT('','3D')
);
#43981=(
LENGTH_UNIT()
NAMED_UNIT(*)
SI_UNIT(.CENTI.,.METRE.)
);
#43983=(
NAMED_UNIT(*)
PLANE_ANGLE_UNIT()
SI_UNIT($,.RADIAN.)
);
#43984=(
NAMED_UNIT(*)
SI_UNIT($,.STERADIAN.)
SOLID_ANGLE_UNIT()
);
#43999=SHAPE_DEFINITION_REPRESENTATION(#44017,#44069);
#44017=PRODUCT_DEFINITION_SHAPE('',$,#44088);
#44069=SHAPE_REPRESENTATION('',(#12053),#43976);
#44073=PRODUCT_DEFINITION_CONTEXT('part definition',#44129,'design');
#44088=PRODUCT_DEFINITION('Socket head cap screw M4x12',
'Socket head cap screw M4x12',#44106,#44073);
#44106=PRODUCT_DEFINITION_FORMATION('',$,#44145);
#44129=APPLICATION_CONTEXT(
'Core Data for Automotive Mechanical Design Process');
#44130=PRODUCT_CONTEXT('part definition',#44129,'mechanical');
#44145=PRODUCT('Socket head cap screw M4x12',
'Socket head cap screw M4x12',$,(#44130));
#44160=PRESENTATION_STYLE_ASSIGNMENT((#44172));
#44172=SURFACE_STYLE_USAGE(.BOTH.,#44184);
#44184=SURFACE_SIDE_STYLE('',(#44196));
#44196=SURFACE_STYLE_FILL_AREA(#44208);
#44208=FILL_AREA_STYLE('Dark gray',(#44220));
#44220=FILL_AREA_STYLE_COLOUR('Dark gray',#44232);
#44232=COLOUR_RGB('Dark gray',0.250980392156863,0.282352941176471,0.32156862745098);
ENDSEC;
END-ISO-10303-21;
